ISO-10303-21;
HEADER;
/* Generated by software containing ST-Developer
 * from STEP Tools, Inc. (www.steptools.com) 
 */

FILE_DESCRIPTION(
/* description */ (''),
/* implementation_level */ '2;1');

FILE_NAME(
/* name */ 'Base.step',
/* time_stamp */ '2026-10-19T01:30:23+06:00',
/* author */ (''),
/* organization */ (''),
/* preprocessor_version */ 'ST-DEVELOPER v20.2',
/* originating_system */ 'Autodesk Translation Framework v15.15.0.0',
/* authorisation */ '');

FILE_SCHEMA (('AUTOMOTIVE_DESIGN { 1 0 10303 214 3 1 1 }'));
ENDSEC;

DATA;
#10=MECHANICAL_DESIGN_GEOMETRIC_PRESENTATION_REPRESENTATION('',(#87),#10639);
#67=SHAPE_REPRESENTATION_RELATIONSHIP('SRR','None',#10677,#77);
#77=ADVANCED_BREP_SHAPE_REPRESENTATION('',(#97),#10629);
#87=STYLED_ITEM('',(#10769),#97);
#97=MANIFOLD_SOLID_BREP('Base',#5713);
#107=SPHERICAL_SURFACE('',#5994,0.299999999999998);
#108=SPHERICAL_SURFACE('',#5998,0.3);
#109=SPHERICAL_SURFACE('',#6004,0.299999999999998);
#110=SPHERICAL_SURFACE('',#6014,0.3);
#111=SPHERICAL_SURFACE('',#6030,0.299999999999998);
#112=SPHERICAL_SURFACE('',#6038,0.3);
#113=SPHERICAL_SURFACE('',#6044,0.3);
#114=SPHERICAL_SURFACE('',#6052,0.299999999999994);
#115=SPHERICAL_SURFACE('',#6067,0.299999999999998);
#116=SPHERICAL_SURFACE('',#6075,0.3);
#117=SPHERICAL_SURFACE('',#6081,0.3);
#118=SPHERICAL_SURFACE('',#6085,0.3);
#119=SPHERICAL_SURFACE('',#6089,0.299999999999998);
#120=SPHERICAL_SURFACE('',#6094,0.299999999999998);
#121=SPHERICAL_SURFACE('',#6100,0.299999999999998);
#122=SPHERICAL_SURFACE('',#6104,0.300000000000002);
#163=ELLIPSE('',#5976,0.42426406871193,0.3);
#164=ELLIPSE('',#5977,0.424264068711927,0.3);
#165=ELLIPSE('',#5979,0.42426406871193,0.3);
#166=ELLIPSE('',#5980,0.424264068711927,0.3);
#167=ELLIPSE('',#5982,0.424264068711929,0.3);
#168=ELLIPSE('',#5984,0.424264068711929,0.3);
#169=ELLIPSE('',#5986,0.424264068711929,0.3);
#170=ELLIPSE('',#5988,0.424264068711929,0.3);
#171=ELLIPSE('',#5990,0.424264068711929,0.3);
#172=ELLIPSE('',#5991,0.424264068711929,0.3);
#173=ELLIPSE('',#5993,0.424264068711929,0.3);
#174=ELLIPSE('',#6009,0.424264068711929,0.3);
#175=ELLIPSE('',#6019,0.424264068711929,0.3);
#176=ELLIPSE('',#6131,0.424264068711929,0.3);
#177=ELLIPSE('',#6134,0.424264068711929,0.3);
#178=ELLIPSE('',#6137,0.424264068711929,0.3);
#179=TOROIDAL_SURFACE('',#5844,5.3,0.3);
#180=TOROIDAL_SURFACE('',#5858,5.3,0.3);
#181=TOROIDAL_SURFACE('',#5865,5.3,0.3);
#182=TOROIDAL_SURFACE('',#5874,5.3,0.3);
#183=TOROIDAL_SURFACE('',#5876,1.8,0.3);
#184=TOROIDAL_SURFACE('',#5898,1.8,0.3);
#185=TOROIDAL_SURFACE('',#5903,1.8,0.3);
#186=TOROIDAL_SURFACE('',#5908,1.8,0.3);
#187=TOROIDAL_SURFACE('',#5913,1.8,0.3);
#188=TOROIDAL_SURFACE('',#5918,1.8,0.3);
#189=TOROIDAL_SURFACE('',#5923,1.8,0.3);
#190=TOROIDAL_SURFACE('',#5928,1.8,0.3);
#191=TOROIDAL_SURFACE('',#5934,1.8,0.3);
#192=TOROIDAL_SURFACE('',#5939,1.8,0.3);
#193=TOROIDAL_SURFACE('',#5945,1.8,0.3);
#194=TOROIDAL_SURFACE('',#5950,1.8,0.3);
#195=TOROIDAL_SURFACE('',#5955,1.8,0.3);
#196=TOROIDAL_SURFACE('',#5960,1.8,0.3);
#197=TOROIDAL_SURFACE('',#5965,1.8,0.3);
#198=TOROIDAL_SURFACE('',#5970,1.8,0.3);
#199=TOROIDAL_SURFACE('',#6010,0.599999999999996,0.299999999999998);
#200=TOROIDAL_SURFACE('',#6021,0.600000000000001,0.3);
#201=TOROIDAL_SURFACE('',#6026,0.599999999999996,0.299999999999998);
#202=TOROIDAL_SURFACE('',#6034,0.599999999999996,0.299999999999998);
#203=TOROIDAL_SURFACE('',#6048,0.600000000000001,0.299999999999998);
#204=TOROIDAL_SURFACE('',#6057,0.600000000000001,0.3);
#205=TOROIDAL_SURFACE('',#6062,0.600000000000001,0.3);
#206=TOROIDAL_SURFACE('',#6071,0.599999999999996,0.299999999999998);
#247=FACE_BOUND('',#773,.T.);
#248=FACE_BOUND('',#776,.T.);
#249=FACE_BOUND('',#780,.T.);
#250=FACE_BOUND('',#781,.T.);
#251=FACE_BOUND('',#787,.T.);
#252=FACE_BOUND('',#788,.T.);
#253=FACE_BOUND('',#792,.T.);
#254=FACE_BOUND('',#793,.T.);
#255=FACE_BOUND('',#794,.T.);
#256=FACE_BOUND('',#795,.T.);
#257=FACE_BOUND('',#796,.T.);
#258=FACE_BOUND('',#797,.T.);
#259=FACE_BOUND('',#798,.T.);
#260=FACE_BOUND('',#799,.T.);
#261=FACE_BOUND('',#800,.T.);
#262=FACE_BOUND('',#801,.T.);
#263=FACE_BOUND('',#802,.T.);
#264=FACE_BOUND('',#803,.T.);
#265=FACE_BOUND('',#804,.T.);
#266=FACE_BOUND('',#805,.T.);
#267=FACE_BOUND('',#806,.T.);
#268=FACE_BOUND('',#807,.T.);
#269=FACE_BOUND('',#919,.T.);
#294=PLANE('',#5839);
#295=PLANE('',#5840);
#296=PLANE('',#5841);
#297=PLANE('',#5842);
#298=PLANE('',#5843);
#299=PLANE('',#5849);
#300=PLANE('',#5868);
#301=PLANE('',#5880);
#302=PLANE('',#6139);
#303=PLANE('',#6140);
#304=PLANE('',#6141);
#305=PLANE('',#6142);
#306=PLANE('',#6143);
#307=PLANE('',#6144);
#308=PLANE('',#6145);
#309=PLANE('',#6146);
#310=PLANE('',#6147);
#311=PLANE('',#6148);
#312=PLANE('',#6149);
#313=PLANE('',#6150);
#314=PLANE('',#6151);
#315=PLANE('',#6152);
#316=PLANE('',#6153);
#317=PLANE('',#6154);
#318=PLANE('',#6155);
#319=PLANE('',#6156);
#320=PLANE('',#6157);
#321=PLANE('',#6158);
#322=PLANE('',#6159);
#323=PLANE('',#6160);
#324=PLANE('',#6161);
#325=PLANE('',#6162);
#326=PLANE('',#6163);
#327=PLANE('',#6164);
#328=PLANE('',#6165);
#329=PLANE('',#6166);
#330=PLANE('',#6167);
#331=PLANE('',#6168);
#332=PLANE('',#6169);
#333=PLANE('',#6170);
#334=PLANE('',#6171);
#335=PLANE('',#6172);
#336=PLANE('',#6173);
#383=FACE_OUTER_BOUND('',#770,.T.);
#384=FACE_OUTER_BOUND('',#771,.T.);
#385=FACE_OUTER_BOUND('',#772,.T.);
#386=FACE_OUTER_BOUND('',#774,.T.);
#387=FACE_OUTER_BOUND('',#775,.T.);
#388=FACE_OUTER_BOUND('',#777,.T.);
#389=FACE_OUTER_BOUND('',#778,.T.);
#390=FACE_OUTER_BOUND('',#779,.T.);
#391=FACE_OUTER_BOUND('',#782,.T.);
#392=FACE_OUTER_BOUND('',#783,.T.);
#393=FACE_OUTER_BOUND('',#784,.T.);
#394=FACE_OUTER_BOUND('',#785,.T.);
#395=FACE_OUTER_BOUND('',#786,.T.);
#396=FACE_OUTER_BOUND('',#789,.T.);
#397=FACE_OUTER_BOUND('',#790,.T.);
#398=FACE_OUTER_BOUND('',#791,.T.);
#399=FACE_OUTER_BOUND('',#808,.T.);
#400=FACE_OUTER_BOUND('',#809,.T.);
#401=FACE_OUTER_BOUND('',#810,.T.);
#402=FACE_OUTER_BOUND('',#811,.T.);
#403=FACE_OUTER_BOUND('',#812,.T.);
#404=FACE_OUTER_BOUND('',#813,.T.);
#405=FACE_OUTER_BOUND('',#814,.T.);
#406=FACE_OUTER_BOUND('',#815,.T.);
#407=FACE_OUTER_BOUND('',#816,.T.);
#408=FACE_OUTER_BOUND('',#817,.T.);
#409=FACE_OUTER_BOUND('',#818,.T.);
#410=FACE_OUTER_BOUND('',#819,.T.);
#411=FACE_OUTER_BOUND('',#820,.T.);
#412=FACE_OUTER_BOUND('',#821,.T.);
#413=FACE_OUTER_BOUND('',#822,.T.);
#414=FACE_OUTER_BOUND('',#823,.T.);
#415=FACE_OUTER_BOUND('',#824,.T.);
#416=FACE_OUTER_BOUND('',#825,.T.);
#417=FACE_OUTER_BOUND('',#826,.T.);
#418=FACE_OUTER_BOUND('',#827,.T.);
#419=FACE_OUTER_BOUND('',#828,.T.);
#420=FACE_OUTER_BOUND('',#829,.T.);
#421=FACE_OUTER_BOUND('',#830,.T.);
#422=FACE_OUTER_BOUND('',#831,.T.);
#423=FACE_OUTER_BOUND('',#832,.T.);
#424=FACE_OUTER_BOUND('',#833,.T.);
#425=FACE_OUTER_BOUND('',#834,.T.);
#426=FACE_OUTER_BOUND('',#835,.T.);
#427=FACE_OUTER_BOUND('',#836,.T.);
#428=FACE_OUTER_BOUND('',#837,.T.);
#429=FACE_OUTER_BOUND('',#838,.T.);
#430=FACE_OUTER_BOUND('',#839,.T.);
#431=FACE_OUTER_BOUND('',#840,.T.);
#432=FACE_OUTER_BOUND('',#841,.T.);
#433=FACE_OUTER_BOUND('',#842,.T.);
#434=FACE_OUTER_BOUND('',#843,.T.);
#435=FACE_OUTER_BOUND('',#844,.T.);
#436=FACE_OUTER_BOUND('',#845,.T.);
#437=FACE_OUTER_BOUND('',#846,.T.);
#438=FACE_OUTER_BOUND('',#847,.T.);
#439=FACE_OUTER_BOUND('',#848,.T.);
#440=FACE_OUTER_BOUND('',#849,.T.);
#441=FACE_OUTER_BOUND('',#850,.T.);
#442=FACE_OUTER_BOUND('',#851,.T.);
#443=FACE_OUTER_BOUND('',#852,.T.);
#444=FACE_OUTER_BOUND('',#853,.T.);
#445=FACE_OUTER_BOUND('',#854,.T.);
#446=FACE_OUTER_BOUND('',#855,.T.);
#447=FACE_OUTER_BOUND('',#856,.T.);
#448=FACE_OUTER_BOUND('',#857,.T.);
#449=FACE_OUTER_BOUND('',#858,.T.);
#450=FACE_OUTER_BOUND('',#859,.T.);
#451=FACE_OUTER_BOUND('',#860,.T.);
#452=FACE_OUTER_BOUND('',#861,.T.);
#453=FACE_OUTER_BOUND('',#862,.T.);
#454=FACE_OUTER_BOUND('',#863,.T.);
#455=FACE_OUTER_BOUND('',#864,.T.);
#456=FACE_OUTER_BOUND('',#865,.T.);
#457=FACE_OUTER_BOUND('',#866,.T.);
#458=FACE_OUTER_BOUND('',#867,.T.);
#459=FACE_OUTER_BOUND('',#868,.T.);
#460=FACE_OUTER_BOUND('',#869,.T.);
#461=FACE_OUTER_BOUND('',#870,.T.);
#462=FACE_OUTER_BOUND('',#871,.T.);
#463=FACE_OUTER_BOUND('',#872,.T.);
#464=FACE_OUTER_BOUND('',#873,.T.);
#465=FACE_OUTER_BOUND('',#874,.T.);
#466=FACE_OUTER_BOUND('',#875,.T.);
#467=FACE_OUTER_BOUND('',#876,.T.);
#468=FACE_OUTER_BOUND('',#877,.T.);
#469=FACE_OUTER_BOUND('',#878,.T.);
#470=FACE_OUTER_BOUND('',#879,.T.);
#471=FACE_OUTER_BOUND('',#880,.T.);
#472=FACE_OUTER_BOUND('',#881,.T.);
#473=FACE_OUTER_BOUND('',#882,.T.);
#474=FACE_OUTER_BOUND('',#883,.T.);
#475=FACE_OUTER_BOUND('',#884,.T.);
#476=FACE_OUTER_BOUND('',#885,.T.);
#477=FACE_OUTER_BOUND('',#886,.T.);
#478=FACE_OUTER_BOUND('',#887,.T.);
#479=FACE_OUTER_BOUND('',#888,.T.);
#480=FACE_OUTER_BOUND('',#889,.T.);
#481=FACE_OUTER_BOUND('',#890,.T.);
#482=FACE_OUTER_BOUND('',#891,.T.);
#483=FACE_OUTER_BOUND('',#892,.T.);
#484=FACE_OUTER_BOUND('',#893,.T.);
#485=FACE_OUTER_BOUND('',#894,.T.);
#486=FACE_OUTER_BOUND('',#895,.T.);
#487=FACE_OUTER_BOUND('',#896,.T.);
#488=FACE_OUTER_BOUND('',#897,.T.);
#489=FACE_OUTER_BOUND('',#898,.T.);
#490=FACE_OUTER_BOUND('',#899,.T.);
#491=FACE_OUTER_BOUND('',#900,.T.);
#492=FACE_OUTER_BOUND('',#901,.T.);
#493=FACE_OUTER_BOUND('',#902,.T.);
#494=FACE_OUTER_BOUND('',#903,.T.);
#495=FACE_OUTER_BOUND('',#904,.T.);
#496=FACE_OUTER_BOUND('',#905,.T.);
#497=FACE_OUTER_BOUND('',#906,.T.);
#498=FACE_OUTER_BOUND('',#907,.T.);
#499=FACE_OUTER_BOUND('',#908,.T.);
#500=FACE_OUTER_BOUND('',#909,.T.);
#501=FACE_OUTER_BOUND('',#910,.T.);
#502=FACE_OUTER_BOUND('',#911,.T.);
#503=FACE_OUTER_BOUND('',#912,.T.);
#504=FACE_OUTER_BOUND('',#913,.T.);
#505=FACE_OUTER_BOUND('',#914,.T.);
#506=FACE_OUTER_BOUND('',#915,.T.);
#507=FACE_OUTER_BOUND('',#916,.T.);
#508=FACE_OUTER_BOUND('',#917,.T.);
#509=FACE_OUTER_BOUND('',#918,.T.);
#510=FACE_OUTER_BOUND('',#920,.T.);
#511=FACE_OUTER_BOUND('',#921,.T.);
#512=FACE_OUTER_BOUND('',#922,.T.);
#513=FACE_OUTER_BOUND('',#923,.T.);
#514=FACE_OUTER_BOUND('',#924,.T.);
#515=FACE_OUTER_BOUND('',#925,.T.);
#516=FACE_OUTER_BOUND('',#926,.T.);
#517=FACE_OUTER_BOUND('',#927,.T.);
#518=FACE_OUTER_BOUND('',#928,.T.);
#519=FACE_OUTER_BOUND('',#929,.T.);
#520=FACE_OUTER_BOUND('',#930,.T.);
#521=FACE_OUTER_BOUND('',#931,.T.);
#522=FACE_OUTER_BOUND('',#932,.T.);
#523=FACE_OUTER_BOUND('',#933,.T.);
#524=FACE_OUTER_BOUND('',#934,.T.);
#525=FACE_OUTER_BOUND('',#935,.T.);
#526=FACE_OUTER_BOUND('',#936,.T.);
#527=FACE_OUTER_BOUND('',#937,.T.);
#528=FACE_OUTER_BOUND('',#938,.T.);
#529=FACE_OUTER_BOUND('',#939,.T.);
#530=FACE_OUTER_BOUND('',#940,.T.);
#531=FACE_OUTER_BOUND('',#941,.T.);
#532=FACE_OUTER_BOUND('',#942,.T.);
#533=FACE_OUTER_BOUND('',#943,.T.);
#534=FACE_OUTER_BOUND('',#944,.T.);
#535=FACE_OUTER_BOUND('',#945,.T.);
#536=FACE_OUTER_BOUND('',#946,.T.);
#537=FACE_OUTER_BOUND('',#947,.T.);
#538=FACE_OUTER_BOUND('',#948,.T.);
#539=FACE_OUTER_BOUND('',#949,.T.);
#540=FACE_OUTER_BOUND('',#950,.T.);
#770=EDGE_LOOP('',(#3552,#3553,#3554,#3555));
#771=EDGE_LOOP('',(#3556,#3557,#3558,#3559));
#772=EDGE_LOOP('',(#3560,#3561,#3562,#3563));
#773=EDGE_LOOP('',(#3564));
#774=EDGE_LOOP('',(#3565,#3566,#3567,#3568));
#775=EDGE_LOOP('',(#3569,#3570,#3571,#3572));
#776=EDGE_LOOP('',(#3573));
#777=EDGE_LOOP('',(#3574,#3575,#3576,#3577));
#778=EDGE_LOOP('',(#3578,#3579,#3580,#3581,#3582));
#779=EDGE_LOOP('',(#3583,#3584,#3585,#3586,#3587,#3588,#3589,#3590,#3591,
#3592,#3593,#3594,#3595,#3596,#3597,#3598,#3599,#3600,#3601,#3602,#3603,
#3604,#3605,#3606));
#780=EDGE_LOOP('',(#3607));
#781=EDGE_LOOP('',(#3608));
#782=EDGE_LOOP('',(#3609,#3610,#3611,#3612,#3613,#3614));
#783=EDGE_LOOP('',(#3615,#3616,#3617,#3618,#3619));
#784=EDGE_LOOP('',(#3620,#3621,#3622,#3623,#3624,#3625));
#785=EDGE_LOOP('',(#3626,#3627,#3628,#3629,#3630));
#786=EDGE_LOOP('',(#3631,#3632,#3633,#3634,#3635,#3636,#3637,#3638,#3639,
#3640,#3641,#3642,#3643,#3644,#3645,#3646,#3647,#3648,#3649,#3650,#3651,
#3652,#3653,#3654));
#787=EDGE_LOOP('',(#3655));
#788=EDGE_LOOP('',(#3656));
#789=EDGE_LOOP('',(#3657,#3658,#3659,#3660,#3661));
#790=EDGE_LOOP('',(#3662,#3663,#3664,#3665));
#791=EDGE_LOOP('',(#3666,#3667,#3668,#3669));
#792=EDGE_LOOP('',(#3670));
#793=EDGE_LOOP('',(#3671));
#794=EDGE_LOOP('',(#3672));
#795=EDGE_LOOP('',(#3673));
#796=EDGE_LOOP('',(#3674));
#797=EDGE_LOOP('',(#3675));
#798=EDGE_LOOP('',(#3676));
#799=EDGE_LOOP('',(#3677));
#800=EDGE_LOOP('',(#3678));
#801=EDGE_LOOP('',(#3679));
#802=EDGE_LOOP('',(#3680));
#803=EDGE_LOOP('',(#3681));
#804=EDGE_LOOP('',(#3682));
#805=EDGE_LOOP('',(#3683));
#806=EDGE_LOOP('',(#3684));
#807=EDGE_LOOP('',(#3685));
#808=EDGE_LOOP('',(#3686,#3687,#3688,#3689));
#809=EDGE_LOOP('',(#3690,#3691,#3692,#3693));
#810=EDGE_LOOP('',(#3694,#3695,#3696,#3697));
#811=EDGE_LOOP('',(#3698,#3699,#3700,#3701));
#812=EDGE_LOOP('',(#3702,#3703,#3704,#3705));
#813=EDGE_LOOP('',(#3706,#3707,#3708,#3709));
#814=EDGE_LOOP('',(#3710,#3711,#3712,#3713));
#815=EDGE_LOOP('',(#3714,#3715,#3716,#3717));
#816=EDGE_LOOP('',(#3718,#3719,#3720,#3721));
#817=EDGE_LOOP('',(#3722,#3723,#3724,#3725));
#818=EDGE_LOOP('',(#3726,#3727,#3728,#3729));
#819=EDGE_LOOP('',(#3730,#3731,#3732,#3733));
#820=EDGE_LOOP('',(#3734,#3735,#3736,#3737));
#821=EDGE_LOOP('',(#3738,#3739,#3740,#3741,#3742));
#822=EDGE_LOOP('',(#3743,#3744,#3745,#3746,#3747));
#823=EDGE_LOOP('',(#3748,#3749,#3750,#3751));
#824=EDGE_LOOP('',(#3752,#3753,#3754,#3755));
#825=EDGE_LOOP('',(#3756,#3757,#3758,#3759,#3760));
#826=EDGE_LOOP('',(#3761,#3762,#3763,#3764,#3765));
#827=EDGE_LOOP('',(#3766,#3767,#3768,#3769));
#828=EDGE_LOOP('',(#3770,#3771,#3772,#3773));
#829=EDGE_LOOP('',(#3774,#3775,#3776,#3777));
#830=EDGE_LOOP('',(#3778,#3779,#3780,#3781));
#831=EDGE_LOOP('',(#3782,#3783,#3784,#3785));
#832=EDGE_LOOP('',(#3786,#3787,#3788,#3789));
#833=EDGE_LOOP('',(#3790,#3791,#3792,#3793));
#834=EDGE_LOOP('',(#3794,#3795,#3796,#3797));
#835=EDGE_LOOP('',(#3798,#3799,#3800,#3801));
#836=EDGE_LOOP('',(#3802,#3803,#3804,#3805));
#837=EDGE_LOOP('',(#3806,#3807,#3808,#3809));
#838=EDGE_LOOP('',(#3810,#3811,#3812,#3813));
#839=EDGE_LOOP('',(#3814,#3815,#3816,#3817));
#840=EDGE_LOOP('',(#3818,#3819,#3820,#3821));
#841=EDGE_LOOP('',(#3822,#3823,#3824,#3825));
#842=EDGE_LOOP('',(#3826,#3827,#3828,#3829));
#843=EDGE_LOOP('',(#3830,#3831,#3832,#3833));
#844=EDGE_LOOP('',(#3834,#3835,#3836,#3837));
#845=EDGE_LOOP('',(#3838,#3839,#3840,#3841));
#846=EDGE_LOOP('',(#3842,#3843,#3844,#3845));
#847=EDGE_LOOP('',(#3846,#3847,#3848));
#848=EDGE_LOOP('',(#3849,#3850,#3851));
#849=EDGE_LOOP('',(#3852,#3853,#3854,#3855));
#850=EDGE_LOOP('',(#3856,#3857,#3858,#3859));
#851=EDGE_LOOP('',(#3860,#3861,#3862));
#852=EDGE_LOOP('',(#3863,#3864,#3865,#3866));
#853=EDGE_LOOP('',(#3867,#3868,#3869,#3870));
#854=EDGE_LOOP('',(#3871,#3872,#3873));
#855=EDGE_LOOP('',(#3874,#3875,#3876,#3877));
#856=EDGE_LOOP('',(#3878,#3879,#3880,#3881));
#857=EDGE_LOOP('',(#3882,#3883,#3884,#3885));
#858=EDGE_LOOP('',(#3886,#3887,#3888,#3889));
#859=EDGE_LOOP('',(#3890,#3891,#3892,#3893));
#860=EDGE_LOOP('',(#3894,#3895,#3896));
#861=EDGE_LOOP('',(#3897,#3898,#3899,#3900));
#862=EDGE_LOOP('',(#3901,#3902,#3903));
#863=EDGE_LOOP('',(#3904,#3905,#3906,#3907));
#864=EDGE_LOOP('',(#3908,#3909,#3910,#3911));
#865=EDGE_LOOP('',(#3912,#3913,#3914));
#866=EDGE_LOOP('',(#3915,#3916,#3917,#3918));
#867=EDGE_LOOP('',(#3919,#3920,#3921));
#868=EDGE_LOOP('',(#3922,#3923,#3924,#3925));
#869=EDGE_LOOP('',(#3926,#3927,#3928,#3929));
#870=EDGE_LOOP('',(#3930,#3931,#3932,#3933));
#871=EDGE_LOOP('',(#3934,#3935,#3936,#3937));
#872=EDGE_LOOP('',(#3938,#3939,#3940,#3941));
#873=EDGE_LOOP('',(#3942,#3943,#3944));
#874=EDGE_LOOP('',(#3945,#3946,#3947,#3948));
#875=EDGE_LOOP('',(#3949,#3950,#3951));
#876=EDGE_LOOP('',(#3952,#3953,#3954,#3955));
#877=EDGE_LOOP('',(#3956,#3957,#3958,#3959));
#878=EDGE_LOOP('',(#3960,#3961,#3962));
#879=EDGE_LOOP('',(#3963,#3964,#3965));
#880=EDGE_LOOP('',(#3966,#3967,#3968));
#881=EDGE_LOOP('',(#3969,#3970,#3971,#3972));
#882=EDGE_LOOP('',(#3973,#3974,#3975));
#883=EDGE_LOOP('',(#3976,#3977,#3978,#3979));
#884=EDGE_LOOP('',(#3980,#3981,#3982,#3983));
#885=EDGE_LOOP('',(#3984,#3985,#3986));
#886=EDGE_LOOP('',(#3987,#3988,#3989));
#887=EDGE_LOOP('',(#3990,#3991,#3992,#3993));
#888=EDGE_LOOP('',(#3994,#3995,#3996,#3997));
#889=EDGE_LOOP('',(#3998,#3999,#4000,#4001));
#890=EDGE_LOOP('',(#4002,#4003,#4004,#4005));
#891=EDGE_LOOP('',(#4006,#4007,#4008,#4009));
#892=EDGE_LOOP('',(#4010,#4011,#4012,#4013));
#893=EDGE_LOOP('',(#4014,#4015,#4016,#4017));
#894=EDGE_LOOP('',(#4018,#4019,#4020,#4021));
#895=EDGE_LOOP('',(#4022,#4023,#4024,#4025));
#896=EDGE_LOOP('',(#4026,#4027,#4028,#4029));
#897=EDGE_LOOP('',(#4030,#4031,#4032,#4033));
#898=EDGE_LOOP('',(#4034,#4035,#4036,#4037));
#899=EDGE_LOOP('',(#4038,#4039,#4040,#4041));
#900=EDGE_LOOP('',(#4042,#4043,#4044,#4045));
#901=EDGE_LOOP('',(#4046,#4047,#4048,#4049));
#902=EDGE_LOOP('',(#4050,#4051,#4052,#4053));
#903=EDGE_LOOP('',(#4054,#4055,#4056,#4057));
#904=EDGE_LOOP('',(#4058,#4059,#4060,#4061));
#905=EDGE_LOOP('',(#4062,#4063,#4064,#4065));
#906=EDGE_LOOP('',(#4066,#4067,#4068,#4069));
#907=EDGE_LOOP('',(#4070,#4071,#4072,#4073));
#908=EDGE_LOOP('',(#4074,#4075,#4076,#4077));
#909=EDGE_LOOP('',(#4078,#4079,#4080,#4081));
#910=EDGE_LOOP('',(#4082,#4083,#4084,#4085));
#911=EDGE_LOOP('',(#4086,#4087,#4088,#4089));
#912=EDGE_LOOP('',(#4090,#4091,#4092,#4093));
#913=EDGE_LOOP('',(#4094,#4095,#4096,#4097));
#914=EDGE_LOOP('',(#4098,#4099,#4100,#4101));
#915=EDGE_LOOP('',(#4102,#4103,#4104,#4105));
#916=EDGE_LOOP('',(#4106,#4107,#4108,#4109));
#917=EDGE_LOOP('',(#4110,#4111,#4112,#4113));
#918=EDGE_LOOP('',(#4114,#4115,#4116,#4117));
#919=EDGE_LOOP('',(#4118,#4119,#4120,#4121));
#920=EDGE_LOOP('',(#4122,#4123,#4124,#4125));
#921=EDGE_LOOP('',(#4126,#4127,#4128,#4129));
#922=EDGE_LOOP('',(#4130,#4131,#4132,#4133));
#923=EDGE_LOOP('',(#4134,#4135,#4136,#4137));
#924=EDGE_LOOP('',(#4138,#4139,#4140,#4141));
#925=EDGE_LOOP('',(#4142,#4143,#4144,#4145));
#926=EDGE_LOOP('',(#4146,#4147,#4148,#4149));
#927=EDGE_LOOP('',(#4150,#4151,#4152,#4153));
#928=EDGE_LOOP('',(#4154,#4155,#4156,#4157));
#929=EDGE_LOOP('',(#4158,#4159,#4160,#4161));
#930=EDGE_LOOP('',(#4162,#4163,#4164,#4165));
#931=EDGE_LOOP('',(#4166,#4167,#4168,#4169));
#932=EDGE_LOOP('',(#4170,#4171,#4172,#4173));
#933=EDGE_LOOP('',(#4174,#4175,#4176,#4177));
#934=EDGE_LOOP('',(#4178,#4179,#4180,#4181));
#935=EDGE_LOOP('',(#4182));
#936=EDGE_LOOP('',(#4183));
#937=EDGE_LOOP('',(#4184));
#938=EDGE_LOOP('',(#4185));
#939=EDGE_LOOP('',(#4186));
#940=EDGE_LOOP('',(#4187));
#941=EDGE_LOOP('',(#4188));
#942=EDGE_LOOP('',(#4189));
#943=EDGE_LOOP('',(#4190));
#944=EDGE_LOOP('',(#4191));
#945=EDGE_LOOP('',(#4192));
#946=EDGE_LOOP('',(#4193));
#947=EDGE_LOOP('',(#4194));
#948=EDGE_LOOP('',(#4195));
#949=EDGE_LOOP('',(#4196));
#950=EDGE_LOOP('',(#4197));
#1204=LINE('',#8756,#1534);
#1205=LINE('',#8761,#1535);
#1206=LINE('',#8763,#1536);
#1207=LINE('',#8765,#1537);
#1208=LINE('',#8766,#1538);
#1209=LINE('',#8769,#1539);
#1210=LINE('',#8771,#1540);
#1211=LINE('',#8772,#1541);
#1212=LINE('',#8775,#1542);
#1213=LINE('',#8777,#1543);
#1214=LINE('',#8778,#1544);
#1215=LINE('',#8780,#1545);
#1216=LINE('',#8781,#1546);
#1217=LINE('',#8794,#1547);
#1218=LINE('',#8796,#1548);
#1219=LINE('',#8800,#1549);
#1220=LINE('',#8802,#1550);
#1221=LINE('',#8806,#1551);
#1222=LINE('',#8808,#1552);
#1223=LINE('',#8810,#1553);
#1224=LINE('',#8812,#1554);
#1225=LINE('',#8814,#1555);
#1226=LINE('',#8816,#1556);
#1227=LINE('',#8818,#1557);
#1228=LINE('',#8820,#1558);
#1229=LINE('',#8822,#1559);
#1230=LINE('',#8824,#1560);
#1231=LINE('',#8826,#1561);
#1232=LINE('',#8830,#1562);
#1233=LINE('',#8832,#1563);
#1234=LINE('',#8836,#1564);
#1235=LINE('',#8838,#1565);
#1236=LINE('',#8839,#1566);
#1237=LINE('',#8844,#1567);
#1238=LINE('',#8856,#1568);
#1239=LINE('',#8869,#1569);
#1240=LINE('',#8871,#1570);
#1241=LINE('',#8873,#1571);
#1242=LINE('',#8875,#1572);
#1243=LINE('',#8877,#1573);
#1244=LINE('',#8881,#1574);
#1245=LINE('',#8883,#1575);
#1246=LINE('',#8887,#1576);
#1247=LINE('',#8889,#1577);
#1248=LINE('',#8891,#1578);
#1249=LINE('',#8893,#1579);
#1250=LINE('',#8895,#1580);
#1251=LINE('',#8897,#1581);
#1252=LINE('',#8899,#1582);
#1253=LINE('',#8901,#1583);
#1254=LINE('',#8903,#1584);
#1255=LINE('',#8905,#1585);
#1256=LINE('',#8907,#1586);
#1257=LINE('',#8911,#1587);
#1258=LINE('',#8912,#1588);
#1259=LINE('',#8926,#1589);
#1260=LINE('',#8928,#1590);
#1261=LINE('',#8930,#1591);
#1262=LINE('',#8931,#1592);
#1263=LINE('',#8964,#1593);
#1264=LINE('',#8972,#1594);
#1265=LINE('',#8980,#1595);
#1266=LINE('',#8988,#1596);
#1267=LINE('',#8996,#1597);
#1268=LINE('',#9004,#1598);
#1269=LINE('',#9012,#1599);
#1270=LINE('',#9022,#1600);
#1271=LINE('',#9030,#1601);
#1272=LINE('',#9040,#1602);
#1273=LINE('',#9048,#1603);
#1274=LINE('',#9056,#1604);
#1275=LINE('',#9064,#1605);
#1276=LINE('',#9072,#1606);
#1277=LINE('',#9080,#1607);
#1278=LINE('',#9088,#1608);
#1279=LINE('',#9094,#1609);
#1280=LINE('',#9100,#1610);
#1281=LINE('',#9105,#1611);
#1282=LINE('',#9109,#1612);
#1283=LINE('',#9113,#1613);
#1284=LINE('',#9117,#1614);
#1285=LINE('',#9121,#1615);
#1286=LINE('',#9127,#1616);
#1287=LINE('',#9141,#1617);
#1288=LINE('',#9142,#1618);
#1289=LINE('',#9144,#1619);
#1290=LINE('',#9153,#1620);
#1291=LINE('',#9169,#1621);
#1292=LINE('',#9172,#1622);
#1293=LINE('',#9173,#1623);
#1294=LINE('',#9181,#1624);
#1295=LINE('',#9207,#1625);
#1296=LINE('',#9208,#1626);
#1297=LINE('',#9210,#1627);
#1298=LINE('',#9230,#1628);
#1299=LINE('',#9231,#1629);
#1300=LINE('',#9239,#1630);
#1301=LINE('',#9247,#1631);
#1302=LINE('',#9267,#1632);
#1303=LINE('',#9268,#1633);
#1304=LINE('',#9270,#1634);
#1305=LINE('',#9289,#1635);
#1306=LINE('',#9290,#1636);
#1307=LINE('',#9297,#1637);
#1308=LINE('',#9299,#1638);
#1309=LINE('',#9311,#1639);
#1310=LINE('',#9314,#1640);
#1311=LINE('',#9316,#1641);
#1312=LINE('',#9319,#1642);
#1313=LINE('',#9321,#1643);
#1314=LINE('',#9323,#1644);
#1315=LINE('',#9325,#1645);
#1316=LINE('',#9327,#1646);
#1317=LINE('',#9328,#1647);
#1318=LINE('',#9330,#1648);
#1319=LINE('',#9332,#1649);
#1320=LINE('',#9333,#1650);
#1321=LINE('',#9335,#1651);
#1322=LINE('',#9337,#1652);
#1323=LINE('',#9339,#1653);
#1324=LINE('',#9341,#1654);
#1325=LINE('',#9343,#1655);
#1326=LINE('',#9344,#1656);
#1327=LINE('',#9346,#1657);
#1328=LINE('',#9348,#1658);
#1329=LINE('',#9350,#1659);
#1330=LINE('',#9351,#1660);
#1331=LINE('',#9353,#1661);
#1332=LINE('',#9355,#1662);
#1333=LINE('',#9358,#1663);
#1334=LINE('',#9361,#1664);
#1335=LINE('',#9364,#1665);
#1336=LINE('',#9367,#1666);
#1337=LINE('',#9370,#1667);
#1338=LINE('',#9373,#1668);
#1339=LINE('',#9375,#1669);
#1340=LINE('',#9376,#1670);
#1341=LINE('',#9378,#1671);
#1342=LINE('',#9380,#1672);
#1343=LINE('',#9382,#1673);
#1344=LINE('',#9384,#1674);
#1345=LINE('',#9386,#1675);
#1346=LINE('',#9388,#1676);
#1534=VECTOR('',#6704,4.925);
#1535=VECTOR('',#6709,10.);
#1536=VECTOR('',#6710,10.);
#1537=VECTOR('',#6711,10.);
#1538=VECTOR('',#6712,10.);
#1539=VECTOR('',#6715,10.);
#1540=VECTOR('',#6716,10.);
#1541=VECTOR('',#6717,10.);
#1542=VECTOR('',#6720,10.);
#1543=VECTOR('',#6721,10.);
#1544=VECTOR('',#6722,10.);
#1545=VECTOR('',#6725,10.);
#1546=VECTOR('',#6726,10.);
#1547=VECTOR('',#6741,10.);
#1548=VECTOR('',#6742,10.);
#1549=VECTOR('',#6745,10.);
#1550=VECTOR('',#6746,10.);
#1551=VECTOR('',#6749,10.);
#1552=VECTOR('',#6750,10.);
#1553=VECTOR('',#6751,10.);
#1554=VECTOR('',#6752,10.);
#1555=VECTOR('',#6753,10.);
#1556=VECTOR('',#6754,10.);
#1557=VECTOR('',#6755,10.);
#1558=VECTOR('',#6756,10.);
#1559=VECTOR('',#6757,10.);
#1560=VECTOR('',#6758,10.);
#1561=VECTOR('',#6759,10.);
#1562=VECTOR('',#6762,10.);
#1563=VECTOR('',#6763,10.);
#1564=VECTOR('',#6766,10.);
#1565=VECTOR('',#6767,10.);
#1566=VECTOR('',#6768,10.);
#1567=VECTOR('',#6773,5.);
#1568=VECTOR('',#6788,5.);
#1569=VECTOR('',#6803,10.);
#1570=VECTOR('',#6804,10.);
#1571=VECTOR('',#6805,10.);
#1572=VECTOR('',#6806,10.);
#1573=VECTOR('',#6807,10.);
#1574=VECTOR('',#6810,10.);
#1575=VECTOR('',#6811,10.);
#1576=VECTOR('',#6814,10.);
#1577=VECTOR('',#6815,10.);
#1578=VECTOR('',#6816,10.);
#1579=VECTOR('',#6817,10.);
#1580=VECTOR('',#6818,10.);
#1581=VECTOR('',#6819,10.);
#1582=VECTOR('',#6820,10.);
#1583=VECTOR('',#6821,10.);
#1584=VECTOR('',#6822,10.);
#1585=VECTOR('',#6823,10.);
#1586=VECTOR('',#6824,10.);
#1587=VECTOR('',#6827,10.);
#1588=VECTOR('',#6828,10.);
#1589=VECTOR('',#6845,10.);
#1590=VECTOR('',#6846,10.);
#1591=VECTOR('',#6847,10.);
#1592=VECTOR('',#6848,10.);
#1593=VECTOR('',#6881,1.5);
#1594=VECTOR('',#6892,1.5);
#1595=VECTOR('',#6903,1.5);
#1596=VECTOR('',#6914,1.5);
#1597=VECTOR('',#6925,1.5);
#1598=VECTOR('',#6936,1.5);
#1599=VECTOR('',#6947,1.5);
#1600=VECTOR('',#6960,1.5);
#1601=VECTOR('',#6971,1.5);
#1602=VECTOR('',#6984,1.5);
#1603=VECTOR('',#6995,1.5);
#1604=VECTOR('',#7006,1.5);
#1605=VECTOR('',#7017,1.5);
#1606=VECTOR('',#7028,1.5);
#1607=VECTOR('',#7039,1.5);
#1608=VECTOR('',#7050,1.5);
#1609=VECTOR('',#7057,10.);
#1610=VECTOR('',#7064,10.);
#1611=VECTOR('',#7071,10.);
#1612=VECTOR('',#7076,10.);
#1613=VECTOR('',#7081,10.);
#1614=VECTOR('',#7086,10.);
#1615=VECTOR('',#7089,10.);
#1616=VECTOR('',#7098,10.);
#1617=VECTOR('',#7117,10.);
#1618=VECTOR('',#7118,10.);
#1619=VECTOR('',#7121,10.);
#1620=VECTOR('',#7132,10.);
#1621=VECTOR('',#7153,10.);
#1622=VECTOR('',#7158,10.);
#1623=VECTOR('',#7159,10.);
#1624=VECTOR('',#7170,10.);
#1625=VECTOR('',#7205,10.);
#1626=VECTOR('',#7206,10.);
#1627=VECTOR('',#7209,10.);
#1628=VECTOR('',#7236,10.);
#1629=VECTOR('',#7237,10.);
#1630=VECTOR('',#7248,10.);
#1631=VECTOR('',#7259,10.);
#1632=VECTOR('',#7286,10.);
#1633=VECTOR('',#7287,10.);
#1634=VECTOR('',#7290,10.);
#1635=VECTOR('',#7317,10.);
#1636=VECTOR('',#7318,10.);
#1637=VECTOR('',#7329,10.);
#1638=VECTOR('',#7332,10.);
#1639=VECTOR('',#7351,10.);
#1640=VECTOR('',#7356,10.);
#1641=VECTOR('',#7359,10.);
#1642=VECTOR('',#7364,10.);
#1643=VECTOR('',#7367,10.);
#1644=VECTOR('',#7370,10.);
#1645=VECTOR('',#7373,10.);
#1646=VECTOR('',#7376,10.);
#1647=VECTOR('',#7377,10.);
#1648=VECTOR('',#7380,10.);
#1649=VECTOR('',#7383,10.);
#1650=VECTOR('',#7384,10.);
#1651=VECTOR('',#7387,10.);
#1652=VECTOR('',#7390,10.);
#1653=VECTOR('',#7393,10.);
#1654=VECTOR('',#7396,10.);
#1655=VECTOR('',#7399,10.);
#1656=VECTOR('',#7400,10.);
#1657=VECTOR('',#7403,10.);
#1658=VECTOR('',#7406,10.);
#1659=VECTOR('',#7409,10.);
#1660=VECTOR('',#7410,10.);
#1661=VECTOR('',#7413,10.);
#1662=VECTOR('',#7416,10.);
#1663=VECTOR('',#7419,10.);
#1664=VECTOR('',#7424,10.);
#1665=VECTOR('',#7427,10.);
#1666=VECTOR('',#7432,10.);
#1667=VECTOR('',#7435,10.);
#1668=VECTOR('',#7440,10.);
#1669=VECTOR('',#7443,10.);
#1670=VECTOR('',#7444,10.);
#1671=VECTOR('',#7447,10.);
#1672=VECTOR('',#7450,10.);
#1673=VECTOR('',#7453,10.);
#1674=VECTOR('',#7456,10.);
#1675=VECTOR('',#7459,10.);
#1676=VECTOR('',#7462,10.);
#1864=CIRCLE('',#5837,5.13675);
#1865=CIRCLE('',#5838,5.13675);
#1866=CIRCLE('',#5845,5.3);
#1867=CIRCLE('',#5846,0.3);
#1868=CIRCLE('',#5847,5.);
#1869=CIRCLE('',#5848,5.);
#1870=CIRCLE('',#5850,0.599999999999996);
#1871=CIRCLE('',#5851,0.599999999999996);
#1872=CIRCLE('',#5852,0.600000000000001);
#1873=CIRCLE('',#5853,0.600000000000001);
#1874=CIRCLE('',#5854,5.3);
#1875=CIRCLE('',#5856,5.);
#1876=CIRCLE('',#5857,5.);
#1877=CIRCLE('',#5859,5.);
#1878=CIRCLE('',#5860,0.3);
#1879=CIRCLE('',#5861,5.);
#1880=CIRCLE('',#5863,5.);
#1881=CIRCLE('',#5864,5.);
#1882=CIRCLE('',#5866,5.3);
#1883=CIRCLE('',#5867,0.3);
#1884=CIRCLE('',#5869,0.600000000000001);
#1885=CIRCLE('',#5870,0.600000000000001);
#1886=CIRCLE('',#5871,0.599999999999996);
#1887=CIRCLE('',#5872,0.600000000000001);
#1888=CIRCLE('',#5873,5.3);
#1889=CIRCLE('',#5875,0.3);
#1890=CIRCLE('',#5877,1.8);
#1891=CIRCLE('',#5878,0.3);
#1892=CIRCLE('',#5879,1.5);
#1893=CIRCLE('',#5881,1.8);
#1894=CIRCLE('',#5882,1.8);
#1895=CIRCLE('',#5883,1.8);
#1896=CIRCLE('',#5884,1.8);
#1897=CIRCLE('',#5885,1.8);
#1898=CIRCLE('',#5886,1.8);
#1899=CIRCLE('',#5887,1.8);
#1900=CIRCLE('',#5888,1.8);
#1901=CIRCLE('',#5889,1.8);
#1902=CIRCLE('',#5890,1.8);
#1903=CIRCLE('',#5891,1.8);
#1904=CIRCLE('',#5892,1.8);
#1905=CIRCLE('',#5893,1.8);
#1906=CIRCLE('',#5894,1.8);
#1907=CIRCLE('',#5895,1.8);
#1908=CIRCLE('',#5897,1.5);
#1909=CIRCLE('',#5899,0.3);
#1910=CIRCLE('',#5900,1.5);
#1911=CIRCLE('',#5902,1.5);
#1912=CIRCLE('',#5904,0.3);
#1913=CIRCLE('',#5905,1.5);
#1914=CIRCLE('',#5907,1.5);
#1915=CIRCLE('',#5909,0.3);
#1916=CIRCLE('',#5910,1.5);
#1917=CIRCLE('',#5912,1.5);
#1918=CIRCLE('',#5914,0.3);
#1919=CIRCLE('',#5915,1.5);
#1920=CIRCLE('',#5917,1.5);
#1921=CIRCLE('',#5919,0.3);
#1922=CIRCLE('',#5920,1.5);
#1923=CIRCLE('',#5922,1.5);
#1924=CIRCLE('',#5924,0.3);
#1925=CIRCLE('',#5925,1.5);
#1926=CIRCLE('',#5927,1.5);
#1927=CIRCLE('',#5929,0.3);
#1928=CIRCLE('',#5930,1.5);
#1929=CIRCLE('',#5931,1.5);
#1930=CIRCLE('',#5933,1.5);
#1931=CIRCLE('',#5935,0.3);
#1932=CIRCLE('',#5936,1.5);
#1933=CIRCLE('',#5938,1.5);
#1934=CIRCLE('',#5940,0.3);
#1935=CIRCLE('',#5941,1.5);
#1936=CIRCLE('',#5942,1.5);
#1937=CIRCLE('',#5944,1.5);
#1938=CIRCLE('',#5946,0.3);
#1939=CIRCLE('',#5947,1.5);
#1940=CIRCLE('',#5949,1.5);
#1941=CIRCLE('',#5951,0.3);
#1942=CIRCLE('',#5952,1.5);
#1943=CIRCLE('',#5954,1.5);
#1944=CIRCLE('',#5956,0.3);
#1945=CIRCLE('',#5957,1.5);
#1946=CIRCLE('',#5959,1.5);
#1947=CIRCLE('',#5961,0.3);
#1948=CIRCLE('',#5962,1.5);
#1949=CIRCLE('',#5964,1.5);
#1950=CIRCLE('',#5966,0.3);
#1951=CIRCLE('',#5967,1.5);
#1952=CIRCLE('',#5969,1.5);
#1953=CIRCLE('',#5971,0.3);
#1954=CIRCLE('',#5972,1.5);
#1955=CIRCLE('',#5974,1.5);
#1956=CIRCLE('',#5995,0.3);
#1957=CIRCLE('',#5996,0.299999999999998);
#1958=CIRCLE('',#5997,0.299999999999998);
#1959=CIRCLE('',#5999,0.299999999999998);
#1960=CIRCLE('',#6000,0.3);
#1961=CIRCLE('',#6001,0.299999999999998);
#1962=CIRCLE('',#6005,0.3);
#1963=CIRCLE('',#6006,0.299999999999998);
#1964=CIRCLE('',#6007,0.299999999999998);
#1965=CIRCLE('',#6011,0.3);
#1966=CIRCLE('',#6012,0.299999999999998);
#1967=CIRCLE('',#6013,0.299999999999998);
#1968=CIRCLE('',#6015,0.299999999999998);
#1969=CIRCLE('',#6016,0.3);
#1970=CIRCLE('',#6017,0.299999999999998);
#1971=CIRCLE('',#6022,0.299999999999998);
#1972=CIRCLE('',#6023,0.299999999999998);
#1973=CIRCLE('',#6024,0.3);
#1974=CIRCLE('',#6027,0.3);
#1975=CIRCLE('',#6028,0.299999999999998);
#1976=CIRCLE('',#6029,0.299999999999998);
#1977=CIRCLE('',#6031,0.3);
#1978=CIRCLE('',#6032,0.299999999999998);
#1979=CIRCLE('',#6033,0.299999999999998);
#1980=CIRCLE('',#6035,0.3);
#1981=CIRCLE('',#6036,0.299999999999998);
#1982=CIRCLE('',#6037,0.299999999999998);
#1983=CIRCLE('',#6039,0.299999999999998);
#1984=CIRCLE('',#6040,0.3);
#1985=CIRCLE('',#6041,0.299999999999998);
#1986=CIRCLE('',#6045,0.299999999999998);
#1987=CIRCLE('',#6046,0.3);
#1988=CIRCLE('',#6047,0.299999999999998);
#1989=CIRCLE('',#6049,0.3);
#1990=CIRCLE('',#6050,0.299999999999998);
#1991=CIRCLE('',#6051,0.299999999999998);
#1992=CIRCLE('',#6053,0.3);
#1993=CIRCLE('',#6054,0.299999999999994);
#1994=CIRCLE('',#6055,0.299999999999998);
#1995=CIRCLE('',#6058,0.299999999999998);
#1996=CIRCLE('',#6059,0.299999999999998);
#1997=CIRCLE('',#6060,0.3);
#1998=CIRCLE('',#6063,0.299999999999998);
#1999=CIRCLE('',#6064,0.299999999999998);
#2000=CIRCLE('',#6065,0.3);
#2001=CIRCLE('',#6068,0.3);
#2002=CIRCLE('',#6069,0.299999999999998);
#2003=CIRCLE('',#6070,0.299999999999998);
#2004=CIRCLE('',#6072,0.3);
#2005=CIRCLE('',#6073,0.299999999999998);
#2006=CIRCLE('',#6074,0.299999999999998);
#2007=CIRCLE('',#6076,0.299999999999998);
#2008=CIRCLE('',#6077,0.3);
#2009=CIRCLE('',#6078,0.299999999999998);
#2010=CIRCLE('',#6082,0.299999999999998);
#2011=CIRCLE('',#6083,0.3);
#2012=CIRCLE('',#6084,0.299999999999998);
#2013=CIRCLE('',#6086,0.299999999999998);
#2014=CIRCLE('',#6087,0.3);
#2015=CIRCLE('',#6088,0.299999999999998);
#2016=CIRCLE('',#6090,0.3);
#2017=CIRCLE('',#6091,0.299999999999998);
#2018=CIRCLE('',#6092,0.299999999999998);
#2019=CIRCLE('',#6095,0.3);
#2020=CIRCLE('',#6096,0.299999999999998);
#2021=CIRCLE('',#6097,0.299999999999998);
#2022=CIRCLE('',#6101,0.3);
#2023=CIRCLE('',#6102,0.299999999999998);
#2024=CIRCLE('',#6103,0.299999999999998);
#2025=CIRCLE('',#6105,0.299999999999998);
#2026=CIRCLE('',#6106,0.300000000000002);
#2027=CIRCLE('',#6107,0.299999999999998);
#2302=VERTEX_POINT('',#8753);
#2303=VERTEX_POINT('',#8755);
#2304=VERTEX_POINT('',#8759);
#2305=VERTEX_POINT('',#8760);
#2306=VERTEX_POINT('',#8762);
#2307=VERTEX_POINT('',#8764);
#2308=VERTEX_POINT('',#8768);
#2309=VERTEX_POINT('',#8770);
#2310=VERTEX_POINT('',#8774);
#2311=VERTEX_POINT('',#8776);
#2312=VERTEX_POINT('',#8784);
#2313=VERTEX_POINT('',#8786);
#2314=VERTEX_POINT('',#8788);
#2315=VERTEX_POINT('',#8792);
#2316=VERTEX_POINT('',#8793);
#2317=VERTEX_POINT('',#8795);
#2318=VERTEX_POINT('',#8797);
#2319=VERTEX_POINT('',#8799);
#2320=VERTEX_POINT('',#8801);
#2321=VERTEX_POINT('',#8803);
#2322=VERTEX_POINT('',#8805);
#2323=VERTEX_POINT('',#8807);
#2324=VERTEX_POINT('',#8809);
#2325=VERTEX_POINT('',#8811);
#2326=VERTEX_POINT('',#8813);
#2327=VERTEX_POINT('',#8815);
#2328=VERTEX_POINT('',#8817);
#2329=VERTEX_POINT('',#8819);
#2330=VERTEX_POINT('',#8821);
#2331=VERTEX_POINT('',#8823);
#2332=VERTEX_POINT('',#8825);
#2333=VERTEX_POINT('',#8827);
#2334=VERTEX_POINT('',#8829);
#2335=VERTEX_POINT('',#8831);
#2336=VERTEX_POINT('',#8833);
#2337=VERTEX_POINT('',#8835);
#2338=VERTEX_POINT('',#8837);
#2339=VERTEX_POINT('',#8840);
#2340=VERTEX_POINT('',#8843);
#2341=VERTEX_POINT('',#8845);
#2342=VERTEX_POINT('',#8849);
#2343=VERTEX_POINT('',#8850);
#2344=VERTEX_POINT('',#8855);
#2345=VERTEX_POINT('',#8857);
#2346=VERTEX_POINT('',#8861);
#2347=VERTEX_POINT('',#8865);
#2348=VERTEX_POINT('',#8866);
#2349=VERTEX_POINT('',#8868);
#2350=VERTEX_POINT('',#8870);
#2351=VERTEX_POINT('',#8872);
#2352=VERTEX_POINT('',#8874);
#2353=VERTEX_POINT('',#8876);
#2354=VERTEX_POINT('',#8878);
#2355=VERTEX_POINT('',#8880);
#2356=VERTEX_POINT('',#8882);
#2357=VERTEX_POINT('',#8884);
#2358=VERTEX_POINT('',#8886);
#2359=VERTEX_POINT('',#8888);
#2360=VERTEX_POINT('',#8890);
#2361=VERTEX_POINT('',#8892);
#2362=VERTEX_POINT('',#8894);
#2363=VERTEX_POINT('',#8896);
#2364=VERTEX_POINT('',#8898);
#2365=VERTEX_POINT('',#8900);
#2366=VERTEX_POINT('',#8902);
#2367=VERTEX_POINT('',#8904);
#2368=VERTEX_POINT('',#8906);
#2369=VERTEX_POINT('',#8908);
#2370=VERTEX_POINT('',#8910);
#2371=VERTEX_POINT('',#8913);
#2372=VERTEX_POINT('',#8918);
#2373=VERTEX_POINT('',#8920);
#2374=VERTEX_POINT('',#8924);
#2375=VERTEX_POINT('',#8925);
#2376=VERTEX_POINT('',#8927);
#2377=VERTEX_POINT('',#8929);
#2378=VERTEX_POINT('',#8932);
#2379=VERTEX_POINT('',#8934);
#2380=VERTEX_POINT('',#8936);
#2381=VERTEX_POINT('',#8938);
#2382=VERTEX_POINT('',#8940);
#2383=VERTEX_POINT('',#8942);
#2384=VERTEX_POINT('',#8944);
#2385=VERTEX_POINT('',#8946);
#2386=VERTEX_POINT('',#8948);
#2387=VERTEX_POINT('',#8950);
#2388=VERTEX_POINT('',#8952);
#2389=VERTEX_POINT('',#8954);
#2390=VERTEX_POINT('',#8956);
#2391=VERTEX_POINT('',#8958);
#2392=VERTEX_POINT('',#8960);
#2393=VERTEX_POINT('',#8963);
#2394=VERTEX_POINT('',#8967);
#2395=VERTEX_POINT('',#8971);
#2396=VERTEX_POINT('',#8975);
#2397=VERTEX_POINT('',#8979);
#2398=VERTEX_POINT('',#8983);
#2399=VERTEX_POINT('',#8987);
#2400=VERTEX_POINT('',#8991);
#2401=VERTEX_POINT('',#8995);
#2402=VERTEX_POINT('',#8999);
#2403=VERTEX_POINT('',#9003);
#2404=VERTEX_POINT('',#9007);
#2405=VERTEX_POINT('',#9011);
#2406=VERTEX_POINT('',#9015);
#2407=VERTEX_POINT('',#9017);
#2408=VERTEX_POINT('',#9021);
#2409=VERTEX_POINT('',#9025);
#2410=VERTEX_POINT('',#9029);
#2411=VERTEX_POINT('',#9033);
#2412=VERTEX_POINT('',#9035);
#2413=VERTEX_POINT('',#9039);
#2414=VERTEX_POINT('',#9043);
#2415=VERTEX_POINT('',#9047);
#2416=VERTEX_POINT('',#9051);
#2417=VERTEX_POINT('',#9055);
#2418=VERTEX_POINT('',#9059);
#2419=VERTEX_POINT('',#9063);
#2420=VERTEX_POINT('',#9067);
#2421=VERTEX_POINT('',#9071);
#2422=VERTEX_POINT('',#9075);
#2423=VERTEX_POINT('',#9079);
#2424=VERTEX_POINT('',#9083);
#2425=VERTEX_POINT('',#9087);
#2426=VERTEX_POINT('',#9091);
#2427=VERTEX_POINT('',#9093);
#2428=VERTEX_POINT('',#9097);
#2429=VERTEX_POINT('',#9099);
#2430=VERTEX_POINT('',#9103);
#2431=VERTEX_POINT('',#9107);
#2432=VERTEX_POINT('',#9111);
#2433=VERTEX_POINT('',#9115);
#2434=VERTEX_POINT('',#9119);
#2435=VERTEX_POINT('',#9120);
#2436=VERTEX_POINT('',#9125);
#2437=VERTEX_POINT('',#9129);
#2438=VERTEX_POINT('',#9131);
#2439=VERTEX_POINT('',#9135);
#2440=VERTEX_POINT('',#9137);
#2441=VERTEX_POINT('',#9146);
#2442=VERTEX_POINT('',#9147);
#2443=VERTEX_POINT('',#9152);
#2444=VERTEX_POINT('',#9156);
#2445=VERTEX_POINT('',#9157);
#2446=VERTEX_POINT('',#9162);
#2447=VERTEX_POINT('',#9164);
#2448=VERTEX_POINT('',#9168);
#2449=VERTEX_POINT('',#9175);
#2450=VERTEX_POINT('',#9176);
#2451=VERTEX_POINT('',#9183);
#2452=VERTEX_POINT('',#9185);
#2453=VERTEX_POINT('',#9189);
#2454=VERTEX_POINT('',#9191);
#2455=VERTEX_POINT('',#9195);
#2456=VERTEX_POINT('',#9196);
#2457=VERTEX_POINT('',#9201);
#2458=VERTEX_POINT('',#9203);
#2459=VERTEX_POINT('',#9212);
#2460=VERTEX_POINT('',#9214);
#2461=VERTEX_POINT('',#9218);
#2462=VERTEX_POINT('',#9219);
#2463=VERTEX_POINT('',#9224);
#2464=VERTEX_POINT('',#9226);
#2465=VERTEX_POINT('',#9233);
#2466=VERTEX_POINT('',#9234);
#2467=VERTEX_POINT('',#9241);
#2468=VERTEX_POINT('',#9242);
#2469=VERTEX_POINT('',#9249);
#2470=VERTEX_POINT('',#9251);
#2471=VERTEX_POINT('',#9255);
#2472=VERTEX_POINT('',#9256);
#2473=VERTEX_POINT('',#9261);
#2474=VERTEX_POINT('',#9263);
#2475=VERTEX_POINT('',#9272);
#2476=VERTEX_POINT('',#9274);
#2477=VERTEX_POINT('',#9278);
#2478=VERTEX_POINT('',#9283);
#2479=VERTEX_POINT('',#9285);
#2480=VERTEX_POINT('',#9293);
#2481=VERTEX_POINT('',#9302);
#2482=VERTEX_POINT('',#9306);
#2483=VERTEX_POINT('',#9357);
#2484=VERTEX_POINT('',#9363);
#2485=VERTEX_POINT('',#9369);
#2752=EDGE_CURVE('',#2302,#2302,#1864,.T.);
#2753=EDGE_CURVE('',#2302,#2303,#1204,.T.);
#2754=EDGE_CURVE('',#2303,#2303,#1865,.T.);
#2755=EDGE_CURVE('',#2304,#2305,#1205,.T.);
#2756=EDGE_CURVE('',#2304,#2306,#1206,.T.);
#2757=EDGE_CURVE('',#2307,#2306,#1207,.T.);
#2758=EDGE_CURVE('',#2305,#2307,#1208,.T.);
#2759=EDGE_CURVE('',#2305,#2308,#1209,.T.);
#2760=EDGE_CURVE('',#2309,#2307,#1210,.T.);
#2761=EDGE_CURVE('',#2308,#2309,#1211,.T.);
#2762=EDGE_CURVE('',#2308,#2310,#1212,.T.);
#2763=EDGE_CURVE('',#2311,#2309,#1213,.T.);
#2764=EDGE_CURVE('',#2310,#2311,#1214,.T.);
#2765=EDGE_CURVE('',#2310,#2304,#1215,.T.);
#2766=EDGE_CURVE('',#2306,#2311,#1216,.T.);
#2767=EDGE_CURVE('',#2312,#2312,#1866,.T.);
#2768=EDGE_CURVE('',#2312,#2313,#1867,.T.);
#2769=EDGE_CURVE('',#2313,#2314,#1868,.T.);
#2770=EDGE_CURVE('',#2314,#2313,#1869,.T.);
#2771=EDGE_CURVE('',#2315,#2316,#1217,.T.);
#2772=EDGE_CURVE('',#2317,#2315,#1218,.T.);
#2773=EDGE_CURVE('',#2318,#2317,#1870,.T.);
#2774=EDGE_CURVE('',#2319,#2318,#1219,.T.);
#2775=EDGE_CURVE('',#2320,#2319,#1220,.T.);
#2776=EDGE_CURVE('',#2321,#2320,#1871,.T.);
#2777=EDGE_CURVE('',#2322,#2321,#1221,.T.);
#2778=EDGE_CURVE('',#2323,#2322,#1222,.T.);
#2779=EDGE_CURVE('',#2324,#2323,#1223,.T.);
#2780=EDGE_CURVE('',#2325,#2324,#1224,.T.);
#2781=EDGE_CURVE('',#2326,#2325,#1225,.T.);
#2782=EDGE_CURVE('',#2327,#2326,#1226,.T.);
#2783=EDGE_CURVE('',#2328,#2327,#1227,.T.);
#2784=EDGE_CURVE('',#2329,#2328,#1228,.T.);
#2785=EDGE_CURVE('',#2330,#2329,#1229,.T.);
#2786=EDGE_CURVE('',#2331,#2330,#1230,.T.);
#2787=EDGE_CURVE('',#2332,#2331,#1231,.T.);
#2788=EDGE_CURVE('',#2333,#2332,#1872,.T.);
#2789=EDGE_CURVE('',#2334,#2333,#1232,.T.);
#2790=EDGE_CURVE('',#2335,#2334,#1233,.T.);
#2791=EDGE_CURVE('',#2336,#2335,#1873,.T.);
#2792=EDGE_CURVE('',#2337,#2336,#1234,.T.);
#2793=EDGE_CURVE('',#2338,#2337,#1235,.T.);
#2794=EDGE_CURVE('',#2316,#2338,#1236,.T.);
#2795=EDGE_CURVE('',#2339,#2339,#1874,.T.);
#2796=EDGE_CURVE('',#2314,#2340,#1237,.T.);
#2797=EDGE_CURVE('',#2341,#2340,#1875,.T.);
#2798=EDGE_CURVE('',#2340,#2341,#1876,.T.);
#2799=EDGE_CURVE('',#2342,#2343,#1877,.T.);
#2800=EDGE_CURVE('',#2343,#2339,#1878,.T.);
#2801=EDGE_CURVE('',#2343,#2342,#1879,.T.);
#2802=EDGE_CURVE('',#2342,#2344,#1238,.T.);
#2803=EDGE_CURVE('',#2345,#2344,#1880,.T.);
#2804=EDGE_CURVE('',#2344,#2345,#1881,.T.);
#2805=EDGE_CURVE('',#2346,#2346,#1882,.T.);
#2806=EDGE_CURVE('',#2346,#2341,#1883,.T.);
#2807=EDGE_CURVE('',#2347,#2348,#1884,.T.);
#2808=EDGE_CURVE('',#2349,#2347,#1239,.T.);
#2809=EDGE_CURVE('',#2350,#2349,#1240,.T.);
#2810=EDGE_CURVE('',#2351,#2350,#1241,.T.);
#2811=EDGE_CURVE('',#2352,#2351,#1242,.T.);
#2812=EDGE_CURVE('',#2353,#2352,#1243,.T.);
#2813=EDGE_CURVE('',#2354,#2353,#1885,.T.);
#2814=EDGE_CURVE('',#2355,#2354,#1244,.T.);
#2815=EDGE_CURVE('',#2356,#2355,#1245,.T.);
#2816=EDGE_CURVE('',#2357,#2356,#1886,.T.);
#2817=EDGE_CURVE('',#2358,#2357,#1246,.T.);
#2818=EDGE_CURVE('',#2359,#2358,#1247,.T.);
#2819=EDGE_CURVE('',#2360,#2359,#1248,.T.);
#2820=EDGE_CURVE('',#2361,#2360,#1249,.T.);
#2821=EDGE_CURVE('',#2362,#2361,#1250,.T.);
#2822=EDGE_CURVE('',#2363,#2362,#1251,.T.);
#2823=EDGE_CURVE('',#2364,#2363,#1252,.T.);
#2824=EDGE_CURVE('',#2365,#2364,#1253,.T.);
#2825=EDGE_CURVE('',#2366,#2365,#1254,.T.);
#2826=EDGE_CURVE('',#2367,#2366,#1255,.T.);
#2827=EDGE_CURVE('',#2368,#2367,#1256,.T.);
#2828=EDGE_CURVE('',#2369,#2368,#1887,.T.);
#2829=EDGE_CURVE('',#2370,#2369,#1257,.T.);
#2830=EDGE_CURVE('',#2348,#2370,#1258,.T.);
#2831=EDGE_CURVE('',#2371,#2371,#1888,.T.);
#2832=EDGE_CURVE('',#2345,#2371,#1889,.T.);
#2833=EDGE_CURVE('',#2372,#2372,#1890,.T.);
#2834=EDGE_CURVE('',#2372,#2373,#1891,.T.);
#2835=EDGE_CURVE('',#2373,#2373,#1892,.T.);
#2836=EDGE_CURVE('',#2374,#2375,#1259,.T.);
#2837=EDGE_CURVE('',#2376,#2374,#1260,.T.);
#2838=EDGE_CURVE('',#2377,#2376,#1261,.T.);
#2839=EDGE_CURVE('',#2375,#2377,#1262,.T.);
#2840=EDGE_CURVE('',#2378,#2378,#1893,.T.);
#2841=EDGE_CURVE('',#2379,#2379,#1894,.T.);
#2842=EDGE_CURVE('',#2380,#2380,#1895,.T.);
#2843=EDGE_CURVE('',#2381,#2381,#1896,.T.);
#2844=EDGE_CURVE('',#2382,#2382,#1897,.T.);
#2845=EDGE_CURVE('',#2383,#2383,#1898,.T.);
#2846=EDGE_CURVE('',#2384,#2384,#1899,.T.);
#2847=EDGE_CURVE('',#2385,#2385,#1900,.T.);
#2848=EDGE_CURVE('',#2386,#2386,#1901,.T.);
#2849=EDGE_CURVE('',#2387,#2387,#1902,.T.);
#2850=EDGE_CURVE('',#2388,#2388,#1903,.T.);
#2851=EDGE_CURVE('',#2389,#2389,#1904,.T.);
#2852=EDGE_CURVE('',#2390,#2390,#1905,.T.);
#2853=EDGE_CURVE('',#2391,#2391,#1906,.T.);
#2854=EDGE_CURVE('',#2392,#2392,#1907,.T.);
#2855=EDGE_CURVE('',#2373,#2393,#1263,.T.);
#2856=EDGE_CURVE('',#2393,#2393,#1908,.T.);
#2857=EDGE_CURVE('',#2378,#2394,#1909,.T.);
#2858=EDGE_CURVE('',#2394,#2394,#1910,.T.);
#2859=EDGE_CURVE('',#2394,#2395,#1264,.T.);
#2860=EDGE_CURVE('',#2395,#2395,#1911,.T.);
#2861=EDGE_CURVE('',#2392,#2396,#1912,.T.);
#2862=EDGE_CURVE('',#2396,#2396,#1913,.T.);
#2863=EDGE_CURVE('',#2396,#2397,#1265,.T.);
#2864=EDGE_CURVE('',#2397,#2397,#1914,.T.);
#2865=EDGE_CURVE('',#2379,#2398,#1915,.T.);
#2866=EDGE_CURVE('',#2398,#2398,#1916,.T.);
#2867=EDGE_CURVE('',#2398,#2399,#1266,.T.);
#2868=EDGE_CURVE('',#2399,#2399,#1917,.T.);
#2869=EDGE_CURVE('',#2391,#2400,#1918,.T.);
#2870=EDGE_CURVE('',#2400,#2400,#1919,.T.);
#2871=EDGE_CURVE('',#2400,#2401,#1267,.T.);
#2872=EDGE_CURVE('',#2401,#2401,#1920,.T.);
#2873=EDGE_CURVE('',#2380,#2402,#1921,.T.);
#2874=EDGE_CURVE('',#2402,#2402,#1922,.T.);
#2875=EDGE_CURVE('',#2402,#2403,#1268,.T.);
#2876=EDGE_CURVE('',#2403,#2403,#1923,.T.);
#2877=EDGE_CURVE('',#2390,#2404,#1924,.T.);
#2878=EDGE_CURVE('',#2404,#2404,#1925,.T.);
#2879=EDGE_CURVE('',#2404,#2405,#1269,.T.);
#2880=EDGE_CURVE('',#2405,#2405,#1926,.T.);
#2881=EDGE_CURVE('',#2381,#2406,#1927,.T.);
#2882=EDGE_CURVE('',#2406,#2407,#1928,.T.);
#2883=EDGE_CURVE('',#2407,#2406,#1929,.T.);
#2884=EDGE_CURVE('',#2407,#2408,#1270,.T.);
#2885=EDGE_CURVE('',#2408,#2408,#1930,.T.);
#2886=EDGE_CURVE('',#2389,#2409,#1931,.T.);
#2887=EDGE_CURVE('',#2409,#2409,#1932,.T.);
#2888=EDGE_CURVE('',#2409,#2410,#1271,.T.);
#2889=EDGE_CURVE('',#2410,#2410,#1933,.T.);
#2890=EDGE_CURVE('',#2382,#2411,#1934,.T.);
#2891=EDGE_CURVE('',#2411,#2412,#1935,.T.);
#2892=EDGE_CURVE('',#2412,#2411,#1936,.T.);
#2893=EDGE_CURVE('',#2412,#2413,#1272,.T.);
#2894=EDGE_CURVE('',#2413,#2413,#1937,.T.);
#2895=EDGE_CURVE('',#2388,#2414,#1938,.T.);
#2896=EDGE_CURVE('',#2414,#2414,#1939,.T.);
#2897=EDGE_CURVE('',#2414,#2415,#1273,.T.);
#2898=EDGE_CURVE('',#2415,#2415,#1940,.T.);
#2899=EDGE_CURVE('',#2383,#2416,#1941,.T.);
#2900=EDGE_CURVE('',#2416,#2416,#1942,.T.);
#2901=EDGE_CURVE('',#2416,#2417,#1274,.T.);
#2902=EDGE_CURVE('',#2417,#2417,#1943,.T.);
#2903=EDGE_CURVE('',#2387,#2418,#1944,.T.);
#2904=EDGE_CURVE('',#2418,#2418,#1945,.T.);
#2905=EDGE_CURVE('',#2418,#2419,#1275,.T.);
#2906=EDGE_CURVE('',#2419,#2419,#1946,.T.);
#2907=EDGE_CURVE('',#2384,#2420,#1947,.T.);
#2908=EDGE_CURVE('',#2420,#2420,#1948,.T.);
#2909=EDGE_CURVE('',#2420,#2421,#1276,.T.);
#2910=EDGE_CURVE('',#2421,#2421,#1949,.T.);
#2911=EDGE_CURVE('',#2386,#2422,#1950,.T.);
#2912=EDGE_CURVE('',#2422,#2422,#1951,.T.);
#2913=EDGE_CURVE('',#2422,#2423,#1277,.T.);
#2914=EDGE_CURVE('',#2423,#2423,#1952,.T.);
#2915=EDGE_CURVE('',#2385,#2424,#1953,.T.);
#2916=EDGE_CURVE('',#2424,#2424,#1954,.T.);
#2917=EDGE_CURVE('',#2424,#2425,#1278,.T.);
#2918=EDGE_CURVE('',#2425,#2425,#1955,.T.);
#2919=EDGE_CURVE('',#2326,#2426,#163,.T.);
#2920=EDGE_CURVE('',#2426,#2427,#1279,.T.);
#2921=EDGE_CURVE('',#2327,#2427,#164,.T.);
#2922=EDGE_CURVE('',#2362,#2428,#165,.T.);
#2923=EDGE_CURVE('',#2428,#2429,#1280,.T.);
#2924=EDGE_CURVE('',#2363,#2429,#166,.T.);
#2925=EDGE_CURVE('',#2361,#2430,#167,.T.);
#2926=EDGE_CURVE('',#2430,#2428,#1281,.T.);
#2927=EDGE_CURVE('',#2325,#2431,#168,.T.);
#2928=EDGE_CURVE('',#2431,#2426,#1282,.T.);
#2929=EDGE_CURVE('',#2360,#2432,#169,.T.);
#2930=EDGE_CURVE('',#2432,#2430,#1283,.T.);
#2931=EDGE_CURVE('',#2324,#2433,#170,.T.);
#2932=EDGE_CURVE('',#2433,#2431,#1284,.T.);
#2933=EDGE_CURVE('',#2434,#2435,#1285,.T.);
#2934=EDGE_CURVE('',#2435,#2365,#171,.T.);
#2935=EDGE_CURVE('',#2364,#2434,#172,.T.);
#2936=EDGE_CURVE('',#2359,#2436,#173,.T.);
#2937=EDGE_CURVE('',#2436,#2432,#1286,.T.);
#2938=EDGE_CURVE('',#2437,#2331,#1956,.F.);
#2939=EDGE_CURVE('',#2438,#2437,#1957,.F.);
#2940=EDGE_CURVE('',#2331,#2438,#1958,.F.);
#2941=EDGE_CURVE('',#2439,#2358,#1959,.F.);
#2942=EDGE_CURVE('',#2440,#2439,#1960,.F.);
#2943=EDGE_CURVE('',#2358,#2440,#1961,.F.);
#2944=EDGE_CURVE('',#2437,#2440,#1287,.T.);
#2945=EDGE_CURVE('',#2439,#2438,#1288,.T.);
#2946=EDGE_CURVE('',#2440,#2436,#1289,.T.);
#2947=EDGE_CURVE('',#2441,#2442,#1962,.F.);
#2948=EDGE_CURVE('',#2322,#2441,#1963,.F.);
#2949=EDGE_CURVE('',#2442,#2322,#1964,.F.);
#2950=EDGE_CURVE('',#2441,#2443,#1290,.T.);
#2951=EDGE_CURVE('',#2443,#2323,#174,.T.);
#2952=EDGE_CURVE('',#2444,#2445,#1965,.F.);
#2953=EDGE_CURVE('',#2333,#2444,#1966,.T.);
#2954=EDGE_CURVE('',#2445,#2332,#1967,.T.);
#2955=EDGE_CURVE('',#2367,#2446,#1968,.F.);
#2956=EDGE_CURVE('',#2447,#2367,#1969,.F.);
#2957=EDGE_CURVE('',#2446,#2447,#1970,.F.);
#2958=EDGE_CURVE('',#2448,#2447,#1291,.T.);
#2959=EDGE_CURVE('',#2366,#2448,#175,.T.);
#2960=EDGE_CURVE('',#2442,#2446,#1292,.T.);
#2961=EDGE_CURVE('',#2447,#2441,#1293,.T.);
#2962=EDGE_CURVE('',#2449,#2450,#1971,.F.);
#2963=EDGE_CURVE('',#2357,#2449,#1972,.T.);
#2964=EDGE_CURVE('',#2450,#2356,#1973,.T.);
#2965=EDGE_CURVE('',#2449,#2439,#1294,.T.);
#2966=EDGE_CURVE('',#2451,#2320,#1974,.T.);
#2967=EDGE_CURVE('',#2452,#2451,#1975,.F.);
#2968=EDGE_CURVE('',#2321,#2452,#1976,.T.);
#2969=EDGE_CURVE('',#2453,#2334,#1977,.F.);
#2970=EDGE_CURVE('',#2454,#2453,#1978,.F.);
#2971=EDGE_CURVE('',#2334,#2454,#1979,.F.);
#2972=EDGE_CURVE('',#2455,#2456,#1980,.F.);
#2973=EDGE_CURVE('',#2369,#2455,#1981,.T.);
#2974=EDGE_CURVE('',#2456,#2368,#1982,.T.);
#2975=EDGE_CURVE('',#2457,#2355,#1983,.F.);
#2976=EDGE_CURVE('',#2458,#2457,#1984,.F.);
#2977=EDGE_CURVE('',#2355,#2458,#1985,.F.);
#2978=EDGE_CURVE('',#2453,#2458,#1295,.T.);
#2979=EDGE_CURVE('',#2457,#2454,#1296,.T.);
#2980=EDGE_CURVE('',#2458,#2450,#1297,.T.);
#2981=EDGE_CURVE('',#2459,#2319,#1986,.F.);
#2982=EDGE_CURVE('',#2460,#2459,#1987,.F.);
#2983=EDGE_CURVE('',#2319,#2460,#1988,.F.);
#2984=EDGE_CURVE('',#2461,#2462,#1989,.F.);
#2985=EDGE_CURVE('',#2336,#2461,#1990,.T.);
#2986=EDGE_CURVE('',#2462,#2335,#1991,.T.);
#2987=EDGE_CURVE('',#2463,#2370,#1992,.F.);
#2988=EDGE_CURVE('',#2464,#2463,#1993,.F.);
#2989=EDGE_CURVE('',#2370,#2464,#1994,.F.);
#2990=EDGE_CURVE('',#2459,#2464,#1298,.T.);
#2991=EDGE_CURVE('',#2463,#2460,#1299,.T.);
#2992=EDGE_CURVE('',#2465,#2466,#1995,.F.);
#2993=EDGE_CURVE('',#2354,#2465,#1996,.T.);
#2994=EDGE_CURVE('',#2466,#2353,#1997,.T.);
#2995=EDGE_CURVE('',#2465,#2457,#1300,.T.);
#2996=EDGE_CURVE('',#2467,#2468,#1998,.F.);
#2997=EDGE_CURVE('',#2318,#2467,#1999,.T.);
#2998=EDGE_CURVE('',#2468,#2317,#2000,.T.);
#2999=EDGE_CURVE('',#2467,#2459,#1301,.T.);
#3000=EDGE_CURVE('',#2469,#2337,#2001,.F.);
#3001=EDGE_CURVE('',#2470,#2469,#2002,.F.);
#3002=EDGE_CURVE('',#2337,#2470,#2003,.F.);
#3003=EDGE_CURVE('',#2471,#2472,#2004,.F.);
#3004=EDGE_CURVE('',#2347,#2471,#2005,.T.);
#3005=EDGE_CURVE('',#2472,#2348,#2006,.T.);
#3006=EDGE_CURVE('',#2473,#2352,#2007,.F.);
#3007=EDGE_CURVE('',#2474,#2473,#2008,.F.);
#3008=EDGE_CURVE('',#2352,#2474,#2009,.F.);
#3009=EDGE_CURVE('',#2469,#2474,#1302,.T.);
#3010=EDGE_CURVE('',#2473,#2470,#1303,.T.);
#3011=EDGE_CURVE('',#2474,#2466,#1304,.T.);
#3012=EDGE_CURVE('',#2475,#2315,#2010,.F.);
#3013=EDGE_CURVE('',#2476,#2475,#2011,.F.);
#3014=EDGE_CURVE('',#2315,#2476,#2012,.F.);
#3015=EDGE_CURVE('',#2477,#2338,#2013,.F.);
#3016=EDGE_CURVE('',#2376,#2477,#2014,.F.);
#3017=EDGE_CURVE('',#2338,#2376,#2015,.F.);
#3018=EDGE_CURVE('',#2478,#2349,#2016,.F.);
#3019=EDGE_CURVE('',#2479,#2478,#2017,.F.);
#3020=EDGE_CURVE('',#2349,#2479,#2018,.F.);
#3021=EDGE_CURVE('',#2475,#2479,#1305,.T.);
#3022=EDGE_CURVE('',#2478,#2476,#1306,.T.);
#3023=EDGE_CURVE('',#2377,#2351,#2019,.F.);
#3024=EDGE_CURVE('',#2480,#2377,#2020,.F.);
#3025=EDGE_CURVE('',#2351,#2480,#2021,.F.);
#3026=EDGE_CURVE('',#2477,#2480,#1307,.T.);
#3027=EDGE_CURVE('',#2480,#2473,#1308,.T.);
#3028=EDGE_CURVE('',#2374,#2316,#2022,.F.);
#3029=EDGE_CURVE('',#2481,#2374,#2023,.F.);
#3030=EDGE_CURVE('',#2316,#2481,#2024,.F.);
#3031=EDGE_CURVE('',#2482,#2350,#2025,.F.);
#3032=EDGE_CURVE('',#2375,#2482,#2026,.F.);
#3033=EDGE_CURVE('',#2350,#2375,#2027,.F.);
#3034=EDGE_CURVE('',#2482,#2481,#1309,.T.);
#3035=EDGE_CURVE('',#2479,#2482,#1310,.T.);
#3036=EDGE_CURVE('',#2481,#2475,#1311,.T.);
#3037=EDGE_CURVE('',#2471,#2478,#1312,.T.);
#3038=EDGE_CURVE('',#2470,#2477,#1313,.T.);
#3039=EDGE_CURVE('',#2476,#2468,#1314,.T.);
#3040=EDGE_CURVE('',#2464,#2472,#1315,.T.);
#3041=EDGE_CURVE('',#2468,#2471,#1316,.T.);
#3042=EDGE_CURVE('',#2472,#2467,#1317,.T.);
#3043=EDGE_CURVE('',#2461,#2469,#1318,.T.);
#3044=EDGE_CURVE('',#2466,#2461,#1319,.T.);
#3045=EDGE_CURVE('',#2462,#2465,#1320,.T.);
#3046=EDGE_CURVE('',#2455,#2463,#1321,.T.);
#3047=EDGE_CURVE('',#2454,#2462,#1322,.T.);
#3048=EDGE_CURVE('',#2460,#2451,#1323,.T.);
#3049=EDGE_CURVE('',#2446,#2456,#1324,.T.);
#3050=EDGE_CURVE('',#2451,#2455,#1325,.T.);
#3051=EDGE_CURVE('',#2456,#2452,#1326,.T.);
#3052=EDGE_CURVE('',#2444,#2453,#1327,.T.);
#3053=EDGE_CURVE('',#2452,#2442,#1328,.T.);
#3054=EDGE_CURVE('',#2450,#2444,#1329,.T.);
#3055=EDGE_CURVE('',#2445,#2449,#1330,.T.);
#3056=EDGE_CURVE('',#2438,#2445,#1331,.T.);
#3057=EDGE_CURVE('',#2435,#2448,#1332,.T.);
#3058=EDGE_CURVE('',#2483,#2437,#1333,.T.);
#3059=EDGE_CURVE('',#2330,#2483,#176,.T.);
#3060=EDGE_CURVE('',#2443,#2433,#1334,.T.);
#3061=EDGE_CURVE('',#2484,#2483,#1335,.T.);
#3062=EDGE_CURVE('',#2329,#2484,#177,.T.);
#3063=EDGE_CURVE('',#2429,#2434,#1336,.T.);
#3064=EDGE_CURVE('',#2485,#2484,#1337,.T.);
#3065=EDGE_CURVE('',#2328,#2485,#178,.T.);
#3066=EDGE_CURVE('',#2427,#2485,#1338,.T.);
#3067=EDGE_CURVE('',#2432,#2484,#1339,.T.);
#3068=EDGE_CURVE('',#2483,#2436,#1340,.T.);
#3069=EDGE_CURVE('',#2485,#2430,#1341,.T.);
#3070=EDGE_CURVE('',#2428,#2427,#1342,.T.);
#3071=EDGE_CURVE('',#2426,#2429,#1343,.T.);
#3072=EDGE_CURVE('',#2431,#2434,#1344,.T.);
#3073=EDGE_CURVE('',#2443,#2448,#1345,.T.);
#3074=EDGE_CURVE('',#2433,#2435,#1346,.T.);
#3552=ORIENTED_EDGE('',*,*,#2752,.F.);
#3553=ORIENTED_EDGE('',*,*,#2753,.T.);
#3554=ORIENTED_EDGE('',*,*,#2754,.F.);
#3555=ORIENTED_EDGE('',*,*,#2753,.F.);
#3556=ORIENTED_EDGE('',*,*,#2755,.F.);
#3557=ORIENTED_EDGE('',*,*,#2756,.T.);
#3558=ORIENTED_EDGE('',*,*,#2757,.F.);
#3559=ORIENTED_EDGE('',*,*,#2758,.F.);
#3560=ORIENTED_EDGE('',*,*,#2759,.F.);
#3561=ORIENTED_EDGE('',*,*,#2758,.T.);
#3562=ORIENTED_EDGE('',*,*,#2760,.F.);
#3563=ORIENTED_EDGE('',*,*,#2761,.F.);
#3564=ORIENTED_EDGE('',*,*,#2752,.T.);
#3565=ORIENTED_EDGE('',*,*,#2762,.F.);
#3566=ORIENTED_EDGE('',*,*,#2761,.T.);
#3567=ORIENTED_EDGE('',*,*,#2763,.F.);
#3568=ORIENTED_EDGE('',*,*,#2764,.F.);
#3569=ORIENTED_EDGE('',*,*,#2765,.F.);
#3570=ORIENTED_EDGE('',*,*,#2764,.T.);
#3571=ORIENTED_EDGE('',*,*,#2766,.F.);
#3572=ORIENTED_EDGE('',*,*,#2756,.F.);
#3573=ORIENTED_EDGE('',*,*,#2754,.T.);
#3574=ORIENTED_EDGE('',*,*,#2766,.T.);
#3575=ORIENTED_EDGE('',*,*,#2763,.T.);
#3576=ORIENTED_EDGE('',*,*,#2760,.T.);
#3577=ORIENTED_EDGE('',*,*,#2757,.T.);
#3578=ORIENTED_EDGE('',*,*,#2767,.T.);
#3579=ORIENTED_EDGE('',*,*,#2768,.T.);
#3580=ORIENTED_EDGE('',*,*,#2769,.T.);
#3581=ORIENTED_EDGE('',*,*,#2770,.T.);
#3582=ORIENTED_EDGE('',*,*,#2768,.F.);
#3583=ORIENTED_EDGE('',*,*,#2771,.F.);
#3584=ORIENTED_EDGE('',*,*,#2772,.F.);
#3585=ORIENTED_EDGE('',*,*,#2773,.F.);
#3586=ORIENTED_EDGE('',*,*,#2774,.F.);
#3587=ORIENTED_EDGE('',*,*,#2775,.F.);
#3588=ORIENTED_EDGE('',*,*,#2776,.F.);
#3589=ORIENTED_EDGE('',*,*,#2777,.F.);
#3590=ORIENTED_EDGE('',*,*,#2778,.F.);
#3591=ORIENTED_EDGE('',*,*,#2779,.F.);
#3592=ORIENTED_EDGE('',*,*,#2780,.F.);
#3593=ORIENTED_EDGE('',*,*,#2781,.F.);
#3594=ORIENTED_EDGE('',*,*,#2782,.F.);
#3595=ORIENTED_EDGE('',*,*,#2783,.F.);
#3596=ORIENTED_EDGE('',*,*,#2784,.F.);
#3597=ORIENTED_EDGE('',*,*,#2785,.F.);
#3598=ORIENTED_EDGE('',*,*,#2786,.F.);
#3599=ORIENTED_EDGE('',*,*,#2787,.F.);
#3600=ORIENTED_EDGE('',*,*,#2788,.F.);
#3601=ORIENTED_EDGE('',*,*,#2789,.F.);
#3602=ORIENTED_EDGE('',*,*,#2790,.F.);
#3603=ORIENTED_EDGE('',*,*,#2791,.F.);
#3604=ORIENTED_EDGE('',*,*,#2792,.F.);
#3605=ORIENTED_EDGE('',*,*,#2793,.F.);
#3606=ORIENTED_EDGE('',*,*,#2794,.F.);
#3607=ORIENTED_EDGE('',*,*,#2795,.F.);
#3608=ORIENTED_EDGE('',*,*,#2767,.F.);
#3609=ORIENTED_EDGE('',*,*,#2770,.F.);
#3610=ORIENTED_EDGE('',*,*,#2796,.T.);
#3611=ORIENTED_EDGE('',*,*,#2797,.F.);
#3612=ORIENTED_EDGE('',*,*,#2798,.F.);
#3613=ORIENTED_EDGE('',*,*,#2796,.F.);
#3614=ORIENTED_EDGE('',*,*,#2769,.F.);
#3615=ORIENTED_EDGE('',*,*,#2799,.T.);
#3616=ORIENTED_EDGE('',*,*,#2800,.T.);
#3617=ORIENTED_EDGE('',*,*,#2795,.T.);
#3618=ORIENTED_EDGE('',*,*,#2800,.F.);
#3619=ORIENTED_EDGE('',*,*,#2801,.T.);
#3620=ORIENTED_EDGE('',*,*,#2799,.F.);
#3621=ORIENTED_EDGE('',*,*,#2802,.T.);
#3622=ORIENTED_EDGE('',*,*,#2803,.F.);
#3623=ORIENTED_EDGE('',*,*,#2804,.F.);
#3624=ORIENTED_EDGE('',*,*,#2802,.F.);
#3625=ORIENTED_EDGE('',*,*,#2801,.F.);
#3626=ORIENTED_EDGE('',*,*,#2805,.T.);
#3627=ORIENTED_EDGE('',*,*,#2806,.T.);
#3628=ORIENTED_EDGE('',*,*,#2797,.T.);
#3629=ORIENTED_EDGE('',*,*,#2798,.T.);
#3630=ORIENTED_EDGE('',*,*,#2806,.F.);
#3631=ORIENTED_EDGE('',*,*,#2807,.F.);
#3632=ORIENTED_EDGE('',*,*,#2808,.F.);
#3633=ORIENTED_EDGE('',*,*,#2809,.F.);
#3634=ORIENTED_EDGE('',*,*,#2810,.F.);
#3635=ORIENTED_EDGE('',*,*,#2811,.F.);
#3636=ORIENTED_EDGE('',*,*,#2812,.F.);
#3637=ORIENTED_EDGE('',*,*,#2813,.F.);
#3638=ORIENTED_EDGE('',*,*,#2814,.F.);
#3639=ORIENTED_EDGE('',*,*,#2815,.F.);
#3640=ORIENTED_EDGE('',*,*,#2816,.F.);
#3641=ORIENTED_EDGE('',*,*,#2817,.F.);
#3642=ORIENTED_EDGE('',*,*,#2818,.F.);
#3643=ORIENTED_EDGE('',*,*,#2819,.F.);
#3644=ORIENTED_EDGE('',*,*,#2820,.F.);
#3645=ORIENTED_EDGE('',*,*,#2821,.F.);
#3646=ORIENTED_EDGE('',*,*,#2822,.F.);
#3647=ORIENTED_EDGE('',*,*,#2823,.F.);
#3648=ORIENTED_EDGE('',*,*,#2824,.F.);
#3649=ORIENTED_EDGE('',*,*,#2825,.F.);
#3650=ORIENTED_EDGE('',*,*,#2826,.F.);
#3651=ORIENTED_EDGE('',*,*,#2827,.F.);
#3652=ORIENTED_EDGE('',*,*,#2828,.F.);
#3653=ORIENTED_EDGE('',*,*,#2829,.F.);
#3654=ORIENTED_EDGE('',*,*,#2830,.F.);
#3655=ORIENTED_EDGE('',*,*,#2831,.F.);
#3656=ORIENTED_EDGE('',*,*,#2805,.F.);
#3657=ORIENTED_EDGE('',*,*,#2804,.T.);
#3658=ORIENTED_EDGE('',*,*,#2832,.T.);
#3659=ORIENTED_EDGE('',*,*,#2831,.T.);
#3660=ORIENTED_EDGE('',*,*,#2832,.F.);
#3661=ORIENTED_EDGE('',*,*,#2803,.T.);
#3662=ORIENTED_EDGE('',*,*,#2833,.T.);
#3663=ORIENTED_EDGE('',*,*,#2834,.T.);
#3664=ORIENTED_EDGE('',*,*,#2835,.T.);
#3665=ORIENTED_EDGE('',*,*,#2834,.F.);
#3666=ORIENTED_EDGE('',*,*,#2836,.F.);
#3667=ORIENTED_EDGE('',*,*,#2837,.F.);
#3668=ORIENTED_EDGE('',*,*,#2838,.F.);
#3669=ORIENTED_EDGE('',*,*,#2839,.F.);
#3670=ORIENTED_EDGE('',*,*,#2840,.F.);
#3671=ORIENTED_EDGE('',*,*,#2841,.F.);
#3672=ORIENTED_EDGE('',*,*,#2842,.F.);
#3673=ORIENTED_EDGE('',*,*,#2843,.F.);
#3674=ORIENTED_EDGE('',*,*,#2844,.F.);
#3675=ORIENTED_EDGE('',*,*,#2845,.F.);
#3676=ORIENTED_EDGE('',*,*,#2846,.F.);
#3677=ORIENTED_EDGE('',*,*,#2847,.F.);
#3678=ORIENTED_EDGE('',*,*,#2848,.F.);
#3679=ORIENTED_EDGE('',*,*,#2849,.F.);
#3680=ORIENTED_EDGE('',*,*,#2850,.F.);
#3681=ORIENTED_EDGE('',*,*,#2851,.F.);
#3682=ORIENTED_EDGE('',*,*,#2852,.F.);
#3683=ORIENTED_EDGE('',*,*,#2853,.F.);
#3684=ORIENTED_EDGE('',*,*,#2854,.F.);
#3685=ORIENTED_EDGE('',*,*,#2833,.F.);
#3686=ORIENTED_EDGE('',*,*,#2835,.F.);
#3687=ORIENTED_EDGE('',*,*,#2855,.T.);
#3688=ORIENTED_EDGE('',*,*,#2856,.T.);
#3689=ORIENTED_EDGE('',*,*,#2855,.F.);
#3690=ORIENTED_EDGE('',*,*,#2840,.T.);
#3691=ORIENTED_EDGE('',*,*,#2857,.T.);
#3692=ORIENTED_EDGE('',*,*,#2858,.T.);
#3693=ORIENTED_EDGE('',*,*,#2857,.F.);
#3694=ORIENTED_EDGE('',*,*,#2858,.F.);
#3695=ORIENTED_EDGE('',*,*,#2859,.T.);
#3696=ORIENTED_EDGE('',*,*,#2860,.T.);
#3697=ORIENTED_EDGE('',*,*,#2859,.F.);
#3698=ORIENTED_EDGE('',*,*,#2854,.T.);
#3699=ORIENTED_EDGE('',*,*,#2861,.T.);
#3700=ORIENTED_EDGE('',*,*,#2862,.T.);
#3701=ORIENTED_EDGE('',*,*,#2861,.F.);
#3702=ORIENTED_EDGE('',*,*,#2862,.F.);
#3703=ORIENTED_EDGE('',*,*,#2863,.T.);
#3704=ORIENTED_EDGE('',*,*,#2864,.T.);
#3705=ORIENTED_EDGE('',*,*,#2863,.F.);
#3706=ORIENTED_EDGE('',*,*,#2841,.T.);
#3707=ORIENTED_EDGE('',*,*,#2865,.T.);
#3708=ORIENTED_EDGE('',*,*,#2866,.T.);
#3709=ORIENTED_EDGE('',*,*,#2865,.F.);
#3710=ORIENTED_EDGE('',*,*,#2866,.F.);
#3711=ORIENTED_EDGE('',*,*,#2867,.T.);
#3712=ORIENTED_EDGE('',*,*,#2868,.T.);
#3713=ORIENTED_EDGE('',*,*,#2867,.F.);
#3714=ORIENTED_EDGE('',*,*,#2853,.T.);
#3715=ORIENTED_EDGE('',*,*,#2869,.T.);
#3716=ORIENTED_EDGE('',*,*,#2870,.T.);
#3717=ORIENTED_EDGE('',*,*,#2869,.F.);
#3718=ORIENTED_EDGE('',*,*,#2870,.F.);
#3719=ORIENTED_EDGE('',*,*,#2871,.T.);
#3720=ORIENTED_EDGE('',*,*,#2872,.T.);
#3721=ORIENTED_EDGE('',*,*,#2871,.F.);
#3722=ORIENTED_EDGE('',*,*,#2842,.T.);
#3723=ORIENTED_EDGE('',*,*,#2873,.T.);
#3724=ORIENTED_EDGE('',*,*,#2874,.T.);
#3725=ORIENTED_EDGE('',*,*,#2873,.F.);
#3726=ORIENTED_EDGE('',*,*,#2874,.F.);
#3727=ORIENTED_EDGE('',*,*,#2875,.T.);
#3728=ORIENTED_EDGE('',*,*,#2876,.T.);
#3729=ORIENTED_EDGE('',*,*,#2875,.F.);
#3730=ORIENTED_EDGE('',*,*,#2852,.T.);
#3731=ORIENTED_EDGE('',*,*,#2877,.T.);
#3732=ORIENTED_EDGE('',*,*,#2878,.T.);
#3733=ORIENTED_EDGE('',*,*,#2877,.F.);
#3734=ORIENTED_EDGE('',*,*,#2878,.F.);
#3735=ORIENTED_EDGE('',*,*,#2879,.T.);
#3736=ORIENTED_EDGE('',*,*,#2880,.T.);
#3737=ORIENTED_EDGE('',*,*,#2879,.F.);
#3738=ORIENTED_EDGE('',*,*,#2843,.T.);
#3739=ORIENTED_EDGE('',*,*,#2881,.T.);
#3740=ORIENTED_EDGE('',*,*,#2882,.T.);
#3741=ORIENTED_EDGE('',*,*,#2883,.T.);
#3742=ORIENTED_EDGE('',*,*,#2881,.F.);
#3743=ORIENTED_EDGE('',*,*,#2883,.F.);
#3744=ORIENTED_EDGE('',*,*,#2884,.T.);
#3745=ORIENTED_EDGE('',*,*,#2885,.T.);
#3746=ORIENTED_EDGE('',*,*,#2884,.F.);
#3747=ORIENTED_EDGE('',*,*,#2882,.F.);
#3748=ORIENTED_EDGE('',*,*,#2851,.T.);
#3749=ORIENTED_EDGE('',*,*,#2886,.T.);
#3750=ORIENTED_EDGE('',*,*,#2887,.T.);
#3751=ORIENTED_EDGE('',*,*,#2886,.F.);
#3752=ORIENTED_EDGE('',*,*,#2887,.F.);
#3753=ORIENTED_EDGE('',*,*,#2888,.T.);
#3754=ORIENTED_EDGE('',*,*,#2889,.T.);
#3755=ORIENTED_EDGE('',*,*,#2888,.F.);
#3756=ORIENTED_EDGE('',*,*,#2844,.T.);
#3757=ORIENTED_EDGE('',*,*,#2890,.T.);
#3758=ORIENTED_EDGE('',*,*,#2891,.T.);
#3759=ORIENTED_EDGE('',*,*,#2892,.T.);
#3760=ORIENTED_EDGE('',*,*,#2890,.F.);
#3761=ORIENTED_EDGE('',*,*,#2892,.F.);
#3762=ORIENTED_EDGE('',*,*,#2893,.T.);
#3763=ORIENTED_EDGE('',*,*,#2894,.T.);
#3764=ORIENTED_EDGE('',*,*,#2893,.F.);
#3765=ORIENTED_EDGE('',*,*,#2891,.F.);
#3766=ORIENTED_EDGE('',*,*,#2850,.T.);
#3767=ORIENTED_EDGE('',*,*,#2895,.T.);
#3768=ORIENTED_EDGE('',*,*,#2896,.T.);
#3769=ORIENTED_EDGE('',*,*,#2895,.F.);
#3770=ORIENTED_EDGE('',*,*,#2896,.F.);
#3771=ORIENTED_EDGE('',*,*,#2897,.T.);
#3772=ORIENTED_EDGE('',*,*,#2898,.T.);
#3773=ORIENTED_EDGE('',*,*,#2897,.F.);
#3774=ORIENTED_EDGE('',*,*,#2845,.T.);
#3775=ORIENTED_EDGE('',*,*,#2899,.T.);
#3776=ORIENTED_EDGE('',*,*,#2900,.T.);
#3777=ORIENTED_EDGE('',*,*,#2899,.F.);
#3778=ORIENTED_EDGE('',*,*,#2900,.F.);
#3779=ORIENTED_EDGE('',*,*,#2901,.T.);
#3780=ORIENTED_EDGE('',*,*,#2902,.T.);
#3781=ORIENTED_EDGE('',*,*,#2901,.F.);
#3782=ORIENTED_EDGE('',*,*,#2849,.T.);
#3783=ORIENTED_EDGE('',*,*,#2903,.T.);
#3784=ORIENTED_EDGE('',*,*,#2904,.T.);
#3785=ORIENTED_EDGE('',*,*,#2903,.F.);
#3786=ORIENTED_EDGE('',*,*,#2904,.F.);
#3787=ORIENTED_EDGE('',*,*,#2905,.T.);
#3788=ORIENTED_EDGE('',*,*,#2906,.T.);
#3789=ORIENTED_EDGE('',*,*,#2905,.F.);
#3790=ORIENTED_EDGE('',*,*,#2846,.T.);
#3791=ORIENTED_EDGE('',*,*,#2907,.T.);
#3792=ORIENTED_EDGE('',*,*,#2908,.T.);
#3793=ORIENTED_EDGE('',*,*,#2907,.F.);
#3794=ORIENTED_EDGE('',*,*,#2908,.F.);
#3795=ORIENTED_EDGE('',*,*,#2909,.T.);
#3796=ORIENTED_EDGE('',*,*,#2910,.T.);
#3797=ORIENTED_EDGE('',*,*,#2909,.F.);
#3798=ORIENTED_EDGE('',*,*,#2848,.T.);
#3799=ORIENTED_EDGE('',*,*,#2911,.T.);
#3800=ORIENTED_EDGE('',*,*,#2912,.T.);
#3801=ORIENTED_EDGE('',*,*,#2911,.F.);
#3802=ORIENTED_EDGE('',*,*,#2912,.F.);
#3803=ORIENTED_EDGE('',*,*,#2913,.T.);
#3804=ORIENTED_EDGE('',*,*,#2914,.T.);
#3805=ORIENTED_EDGE('',*,*,#2913,.F.);
#3806=ORIENTED_EDGE('',*,*,#2847,.T.);
#3807=ORIENTED_EDGE('',*,*,#2915,.T.);
#3808=ORIENTED_EDGE('',*,*,#2916,.T.);
#3809=ORIENTED_EDGE('',*,*,#2915,.F.);
#3810=ORIENTED_EDGE('',*,*,#2916,.F.);
#3811=ORIENTED_EDGE('',*,*,#2917,.T.);
#3812=ORIENTED_EDGE('',*,*,#2918,.T.);
#3813=ORIENTED_EDGE('',*,*,#2917,.F.);
#3814=ORIENTED_EDGE('',*,*,#2782,.T.);
#3815=ORIENTED_EDGE('',*,*,#2919,.T.);
#3816=ORIENTED_EDGE('',*,*,#2920,.T.);
#3817=ORIENTED_EDGE('',*,*,#2921,.F.);
#3818=ORIENTED_EDGE('',*,*,#2822,.T.);
#3819=ORIENTED_EDGE('',*,*,#2922,.T.);
#3820=ORIENTED_EDGE('',*,*,#2923,.T.);
#3821=ORIENTED_EDGE('',*,*,#2924,.F.);
#3822=ORIENTED_EDGE('',*,*,#2821,.T.);
#3823=ORIENTED_EDGE('',*,*,#2925,.T.);
#3824=ORIENTED_EDGE('',*,*,#2926,.T.);
#3825=ORIENTED_EDGE('',*,*,#2922,.F.);
#3826=ORIENTED_EDGE('',*,*,#2781,.T.);
#3827=ORIENTED_EDGE('',*,*,#2927,.T.);
#3828=ORIENTED_EDGE('',*,*,#2928,.T.);
#3829=ORIENTED_EDGE('',*,*,#2919,.F.);
#3830=ORIENTED_EDGE('',*,*,#2820,.T.);
#3831=ORIENTED_EDGE('',*,*,#2929,.T.);
#3832=ORIENTED_EDGE('',*,*,#2930,.T.);
#3833=ORIENTED_EDGE('',*,*,#2925,.F.);
#3834=ORIENTED_EDGE('',*,*,#2780,.T.);
#3835=ORIENTED_EDGE('',*,*,#2931,.T.);
#3836=ORIENTED_EDGE('',*,*,#2932,.T.);
#3837=ORIENTED_EDGE('',*,*,#2927,.F.);
#3838=ORIENTED_EDGE('',*,*,#2933,.T.);
#3839=ORIENTED_EDGE('',*,*,#2934,.T.);
#3840=ORIENTED_EDGE('',*,*,#2824,.T.);
#3841=ORIENTED_EDGE('',*,*,#2935,.T.);
#3842=ORIENTED_EDGE('',*,*,#2819,.T.);
#3843=ORIENTED_EDGE('',*,*,#2936,.T.);
#3844=ORIENTED_EDGE('',*,*,#2937,.T.);
#3845=ORIENTED_EDGE('',*,*,#2929,.F.);
#3846=ORIENTED_EDGE('',*,*,#2938,.F.);
#3847=ORIENTED_EDGE('',*,*,#2939,.F.);
#3848=ORIENTED_EDGE('',*,*,#2940,.F.);
#3849=ORIENTED_EDGE('',*,*,#2941,.F.);
#3850=ORIENTED_EDGE('',*,*,#2942,.F.);
#3851=ORIENTED_EDGE('',*,*,#2943,.F.);
#3852=ORIENTED_EDGE('',*,*,#2939,.T.);
#3853=ORIENTED_EDGE('',*,*,#2944,.T.);
#3854=ORIENTED_EDGE('',*,*,#2942,.T.);
#3855=ORIENTED_EDGE('',*,*,#2945,.T.);
#3856=ORIENTED_EDGE('',*,*,#2818,.T.);
#3857=ORIENTED_EDGE('',*,*,#2943,.T.);
#3858=ORIENTED_EDGE('',*,*,#2946,.T.);
#3859=ORIENTED_EDGE('',*,*,#2936,.F.);
#3860=ORIENTED_EDGE('',*,*,#2947,.F.);
#3861=ORIENTED_EDGE('',*,*,#2948,.F.);
#3862=ORIENTED_EDGE('',*,*,#2949,.F.);
#3863=ORIENTED_EDGE('',*,*,#2778,.T.);
#3864=ORIENTED_EDGE('',*,*,#2948,.T.);
#3865=ORIENTED_EDGE('',*,*,#2950,.T.);
#3866=ORIENTED_EDGE('',*,*,#2951,.T.);
#3867=ORIENTED_EDGE('',*,*,#2952,.F.);
#3868=ORIENTED_EDGE('',*,*,#2953,.F.);
#3869=ORIENTED_EDGE('',*,*,#2788,.T.);
#3870=ORIENTED_EDGE('',*,*,#2954,.F.);
#3871=ORIENTED_EDGE('',*,*,#2955,.F.);
#3872=ORIENTED_EDGE('',*,*,#2956,.F.);
#3873=ORIENTED_EDGE('',*,*,#2957,.F.);
#3874=ORIENTED_EDGE('',*,*,#2958,.T.);
#3875=ORIENTED_EDGE('',*,*,#2956,.T.);
#3876=ORIENTED_EDGE('',*,*,#2826,.T.);
#3877=ORIENTED_EDGE('',*,*,#2959,.T.);
#3878=ORIENTED_EDGE('',*,*,#2947,.T.);
#3879=ORIENTED_EDGE('',*,*,#2960,.T.);
#3880=ORIENTED_EDGE('',*,*,#2957,.T.);
#3881=ORIENTED_EDGE('',*,*,#2961,.T.);
#3882=ORIENTED_EDGE('',*,*,#2962,.F.);
#3883=ORIENTED_EDGE('',*,*,#2963,.F.);
#3884=ORIENTED_EDGE('',*,*,#2816,.T.);
#3885=ORIENTED_EDGE('',*,*,#2964,.F.);
#3886=ORIENTED_EDGE('',*,*,#2941,.T.);
#3887=ORIENTED_EDGE('',*,*,#2817,.T.);
#3888=ORIENTED_EDGE('',*,*,#2963,.T.);
#3889=ORIENTED_EDGE('',*,*,#2965,.T.);
#3890=ORIENTED_EDGE('',*,*,#2776,.T.);
#3891=ORIENTED_EDGE('',*,*,#2966,.F.);
#3892=ORIENTED_EDGE('',*,*,#2967,.F.);
#3893=ORIENTED_EDGE('',*,*,#2968,.F.);
#3894=ORIENTED_EDGE('',*,*,#2969,.F.);
#3895=ORIENTED_EDGE('',*,*,#2970,.F.);
#3896=ORIENTED_EDGE('',*,*,#2971,.F.);
#3897=ORIENTED_EDGE('',*,*,#2972,.F.);
#3898=ORIENTED_EDGE('',*,*,#2973,.F.);
#3899=ORIENTED_EDGE('',*,*,#2828,.T.);
#3900=ORIENTED_EDGE('',*,*,#2974,.F.);
#3901=ORIENTED_EDGE('',*,*,#2975,.F.);
#3902=ORIENTED_EDGE('',*,*,#2976,.F.);
#3903=ORIENTED_EDGE('',*,*,#2977,.F.);
#3904=ORIENTED_EDGE('',*,*,#2970,.T.);
#3905=ORIENTED_EDGE('',*,*,#2978,.T.);
#3906=ORIENTED_EDGE('',*,*,#2976,.T.);
#3907=ORIENTED_EDGE('',*,*,#2979,.T.);
#3908=ORIENTED_EDGE('',*,*,#2964,.T.);
#3909=ORIENTED_EDGE('',*,*,#2815,.T.);
#3910=ORIENTED_EDGE('',*,*,#2977,.T.);
#3911=ORIENTED_EDGE('',*,*,#2980,.T.);
#3912=ORIENTED_EDGE('',*,*,#2981,.F.);
#3913=ORIENTED_EDGE('',*,*,#2982,.F.);
#3914=ORIENTED_EDGE('',*,*,#2983,.F.);
#3915=ORIENTED_EDGE('',*,*,#2984,.F.);
#3916=ORIENTED_EDGE('',*,*,#2985,.F.);
#3917=ORIENTED_EDGE('',*,*,#2791,.T.);
#3918=ORIENTED_EDGE('',*,*,#2986,.F.);
#3919=ORIENTED_EDGE('',*,*,#2987,.F.);
#3920=ORIENTED_EDGE('',*,*,#2988,.F.);
#3921=ORIENTED_EDGE('',*,*,#2989,.F.);
#3922=ORIENTED_EDGE('',*,*,#2982,.T.);
#3923=ORIENTED_EDGE('',*,*,#2990,.T.);
#3924=ORIENTED_EDGE('',*,*,#2988,.T.);
#3925=ORIENTED_EDGE('',*,*,#2991,.T.);
#3926=ORIENTED_EDGE('',*,*,#2992,.F.);
#3927=ORIENTED_EDGE('',*,*,#2993,.F.);
#3928=ORIENTED_EDGE('',*,*,#2813,.T.);
#3929=ORIENTED_EDGE('',*,*,#2994,.F.);
#3930=ORIENTED_EDGE('',*,*,#2975,.T.);
#3931=ORIENTED_EDGE('',*,*,#2814,.T.);
#3932=ORIENTED_EDGE('',*,*,#2993,.T.);
#3933=ORIENTED_EDGE('',*,*,#2995,.T.);
#3934=ORIENTED_EDGE('',*,*,#2996,.F.);
#3935=ORIENTED_EDGE('',*,*,#2997,.F.);
#3936=ORIENTED_EDGE('',*,*,#2773,.T.);
#3937=ORIENTED_EDGE('',*,*,#2998,.F.);
#3938=ORIENTED_EDGE('',*,*,#2997,.T.);
#3939=ORIENTED_EDGE('',*,*,#2999,.T.);
#3940=ORIENTED_EDGE('',*,*,#2981,.T.);
#3941=ORIENTED_EDGE('',*,*,#2774,.T.);
#3942=ORIENTED_EDGE('',*,*,#3000,.F.);
#3943=ORIENTED_EDGE('',*,*,#3001,.F.);
#3944=ORIENTED_EDGE('',*,*,#3002,.F.);
#3945=ORIENTED_EDGE('',*,*,#3003,.F.);
#3946=ORIENTED_EDGE('',*,*,#3004,.F.);
#3947=ORIENTED_EDGE('',*,*,#2807,.T.);
#3948=ORIENTED_EDGE('',*,*,#3005,.F.);
#3949=ORIENTED_EDGE('',*,*,#3006,.F.);
#3950=ORIENTED_EDGE('',*,*,#3007,.F.);
#3951=ORIENTED_EDGE('',*,*,#3008,.F.);
#3952=ORIENTED_EDGE('',*,*,#3001,.T.);
#3953=ORIENTED_EDGE('',*,*,#3009,.T.);
#3954=ORIENTED_EDGE('',*,*,#3007,.T.);
#3955=ORIENTED_EDGE('',*,*,#3010,.T.);
#3956=ORIENTED_EDGE('',*,*,#2994,.T.);
#3957=ORIENTED_EDGE('',*,*,#2812,.T.);
#3958=ORIENTED_EDGE('',*,*,#3008,.T.);
#3959=ORIENTED_EDGE('',*,*,#3011,.T.);
#3960=ORIENTED_EDGE('',*,*,#3012,.F.);
#3961=ORIENTED_EDGE('',*,*,#3013,.F.);
#3962=ORIENTED_EDGE('',*,*,#3014,.F.);
#3963=ORIENTED_EDGE('',*,*,#3015,.F.);
#3964=ORIENTED_EDGE('',*,*,#3016,.F.);
#3965=ORIENTED_EDGE('',*,*,#3017,.F.);
#3966=ORIENTED_EDGE('',*,*,#3018,.F.);
#3967=ORIENTED_EDGE('',*,*,#3019,.F.);
#3968=ORIENTED_EDGE('',*,*,#3020,.F.);
#3969=ORIENTED_EDGE('',*,*,#3013,.T.);
#3970=ORIENTED_EDGE('',*,*,#3021,.T.);
#3971=ORIENTED_EDGE('',*,*,#3019,.T.);
#3972=ORIENTED_EDGE('',*,*,#3022,.T.);
#3973=ORIENTED_EDGE('',*,*,#3023,.F.);
#3974=ORIENTED_EDGE('',*,*,#3024,.F.);
#3975=ORIENTED_EDGE('',*,*,#3025,.F.);
#3976=ORIENTED_EDGE('',*,*,#3016,.T.);
#3977=ORIENTED_EDGE('',*,*,#3026,.T.);
#3978=ORIENTED_EDGE('',*,*,#3024,.T.);
#3979=ORIENTED_EDGE('',*,*,#2838,.T.);
#3980=ORIENTED_EDGE('',*,*,#3006,.T.);
#3981=ORIENTED_EDGE('',*,*,#2811,.T.);
#3982=ORIENTED_EDGE('',*,*,#3025,.T.);
#3983=ORIENTED_EDGE('',*,*,#3027,.T.);
#3984=ORIENTED_EDGE('',*,*,#3028,.F.);
#3985=ORIENTED_EDGE('',*,*,#3029,.F.);
#3986=ORIENTED_EDGE('',*,*,#3030,.F.);
#3987=ORIENTED_EDGE('',*,*,#3031,.F.);
#3988=ORIENTED_EDGE('',*,*,#3032,.F.);
#3989=ORIENTED_EDGE('',*,*,#3033,.F.);
#3990=ORIENTED_EDGE('',*,*,#3029,.T.);
#3991=ORIENTED_EDGE('',*,*,#2836,.T.);
#3992=ORIENTED_EDGE('',*,*,#3032,.T.);
#3993=ORIENTED_EDGE('',*,*,#3034,.T.);
#3994=ORIENTED_EDGE('',*,*,#3023,.T.);
#3995=ORIENTED_EDGE('',*,*,#2810,.T.);
#3996=ORIENTED_EDGE('',*,*,#3033,.T.);
#3997=ORIENTED_EDGE('',*,*,#2839,.T.);
#3998=ORIENTED_EDGE('',*,*,#3031,.T.);
#3999=ORIENTED_EDGE('',*,*,#2809,.T.);
#4000=ORIENTED_EDGE('',*,*,#3020,.T.);
#4001=ORIENTED_EDGE('',*,*,#3035,.T.);
#4002=ORIENTED_EDGE('',*,*,#3012,.T.);
#4003=ORIENTED_EDGE('',*,*,#2771,.T.);
#4004=ORIENTED_EDGE('',*,*,#3030,.T.);
#4005=ORIENTED_EDGE('',*,*,#3036,.T.);
#4006=ORIENTED_EDGE('',*,*,#3028,.T.);
#4007=ORIENTED_EDGE('',*,*,#2794,.T.);
#4008=ORIENTED_EDGE('',*,*,#3017,.T.);
#4009=ORIENTED_EDGE('',*,*,#2837,.T.);
#4010=ORIENTED_EDGE('',*,*,#3018,.T.);
#4011=ORIENTED_EDGE('',*,*,#2808,.T.);
#4012=ORIENTED_EDGE('',*,*,#3004,.T.);
#4013=ORIENTED_EDGE('',*,*,#3037,.T.);
#4014=ORIENTED_EDGE('',*,*,#3015,.T.);
#4015=ORIENTED_EDGE('',*,*,#2793,.T.);
#4016=ORIENTED_EDGE('',*,*,#3002,.T.);
#4017=ORIENTED_EDGE('',*,*,#3038,.T.);
#4018=ORIENTED_EDGE('',*,*,#2998,.T.);
#4019=ORIENTED_EDGE('',*,*,#2772,.T.);
#4020=ORIENTED_EDGE('',*,*,#3014,.T.);
#4021=ORIENTED_EDGE('',*,*,#3039,.T.);
#4022=ORIENTED_EDGE('',*,*,#2989,.T.);
#4023=ORIENTED_EDGE('',*,*,#3040,.T.);
#4024=ORIENTED_EDGE('',*,*,#3005,.T.);
#4025=ORIENTED_EDGE('',*,*,#2830,.T.);
#4026=ORIENTED_EDGE('',*,*,#2996,.T.);
#4027=ORIENTED_EDGE('',*,*,#3041,.T.);
#4028=ORIENTED_EDGE('',*,*,#3003,.T.);
#4029=ORIENTED_EDGE('',*,*,#3042,.T.);
#4030=ORIENTED_EDGE('',*,*,#3000,.T.);
#4031=ORIENTED_EDGE('',*,*,#2792,.T.);
#4032=ORIENTED_EDGE('',*,*,#2985,.T.);
#4033=ORIENTED_EDGE('',*,*,#3043,.T.);
#4034=ORIENTED_EDGE('',*,*,#2992,.T.);
#4035=ORIENTED_EDGE('',*,*,#3044,.T.);
#4036=ORIENTED_EDGE('',*,*,#2984,.T.);
#4037=ORIENTED_EDGE('',*,*,#3045,.T.);
#4038=ORIENTED_EDGE('',*,*,#2973,.T.);
#4039=ORIENTED_EDGE('',*,*,#3046,.T.);
#4040=ORIENTED_EDGE('',*,*,#2987,.T.);
#4041=ORIENTED_EDGE('',*,*,#2829,.T.);
#4042=ORIENTED_EDGE('',*,*,#2986,.T.);
#4043=ORIENTED_EDGE('',*,*,#2790,.T.);
#4044=ORIENTED_EDGE('',*,*,#2971,.T.);
#4045=ORIENTED_EDGE('',*,*,#3047,.T.);
#4046=ORIENTED_EDGE('',*,*,#2983,.T.);
#4047=ORIENTED_EDGE('',*,*,#3048,.T.);
#4048=ORIENTED_EDGE('',*,*,#2966,.T.);
#4049=ORIENTED_EDGE('',*,*,#2775,.T.);
#4050=ORIENTED_EDGE('',*,*,#2955,.T.);
#4051=ORIENTED_EDGE('',*,*,#3049,.T.);
#4052=ORIENTED_EDGE('',*,*,#2974,.T.);
#4053=ORIENTED_EDGE('',*,*,#2827,.T.);
#4054=ORIENTED_EDGE('',*,*,#2967,.T.);
#4055=ORIENTED_EDGE('',*,*,#3050,.T.);
#4056=ORIENTED_EDGE('',*,*,#2972,.T.);
#4057=ORIENTED_EDGE('',*,*,#3051,.T.);
#4058=ORIENTED_EDGE('',*,*,#2969,.T.);
#4059=ORIENTED_EDGE('',*,*,#2789,.T.);
#4060=ORIENTED_EDGE('',*,*,#2953,.T.);
#4061=ORIENTED_EDGE('',*,*,#3052,.T.);
#4062=ORIENTED_EDGE('',*,*,#2968,.T.);
#4063=ORIENTED_EDGE('',*,*,#3053,.T.);
#4064=ORIENTED_EDGE('',*,*,#2949,.T.);
#4065=ORIENTED_EDGE('',*,*,#2777,.T.);
#4066=ORIENTED_EDGE('',*,*,#2962,.T.);
#4067=ORIENTED_EDGE('',*,*,#3054,.T.);
#4068=ORIENTED_EDGE('',*,*,#2952,.T.);
#4069=ORIENTED_EDGE('',*,*,#3055,.T.);
#4070=ORIENTED_EDGE('',*,*,#2954,.T.);
#4071=ORIENTED_EDGE('',*,*,#2787,.T.);
#4072=ORIENTED_EDGE('',*,*,#2940,.T.);
#4073=ORIENTED_EDGE('',*,*,#3056,.T.);
#4074=ORIENTED_EDGE('',*,*,#3057,.T.);
#4075=ORIENTED_EDGE('',*,*,#2959,.F.);
#4076=ORIENTED_EDGE('',*,*,#2825,.T.);
#4077=ORIENTED_EDGE('',*,*,#2934,.F.);
#4078=ORIENTED_EDGE('',*,*,#3058,.T.);
#4079=ORIENTED_EDGE('',*,*,#2938,.T.);
#4080=ORIENTED_EDGE('',*,*,#2786,.T.);
#4081=ORIENTED_EDGE('',*,*,#3059,.T.);
#4082=ORIENTED_EDGE('',*,*,#2779,.T.);
#4083=ORIENTED_EDGE('',*,*,#2951,.F.);
#4084=ORIENTED_EDGE('',*,*,#3060,.T.);
#4085=ORIENTED_EDGE('',*,*,#2931,.F.);
#4086=ORIENTED_EDGE('',*,*,#3061,.T.);
#4087=ORIENTED_EDGE('',*,*,#3059,.F.);
#4088=ORIENTED_EDGE('',*,*,#2785,.T.);
#4089=ORIENTED_EDGE('',*,*,#3062,.T.);
#4090=ORIENTED_EDGE('',*,*,#3063,.T.);
#4091=ORIENTED_EDGE('',*,*,#2935,.F.);
#4092=ORIENTED_EDGE('',*,*,#2823,.T.);
#4093=ORIENTED_EDGE('',*,*,#2924,.T.);
#4094=ORIENTED_EDGE('',*,*,#3064,.T.);
#4095=ORIENTED_EDGE('',*,*,#3062,.F.);
#4096=ORIENTED_EDGE('',*,*,#2784,.T.);
#4097=ORIENTED_EDGE('',*,*,#3065,.T.);
#4098=ORIENTED_EDGE('',*,*,#3066,.T.);
#4099=ORIENTED_EDGE('',*,*,#3065,.F.);
#4100=ORIENTED_EDGE('',*,*,#2783,.T.);
#4101=ORIENTED_EDGE('',*,*,#2921,.T.);
#4102=ORIENTED_EDGE('',*,*,#3061,.F.);
#4103=ORIENTED_EDGE('',*,*,#3067,.F.);
#4104=ORIENTED_EDGE('',*,*,#2937,.F.);
#4105=ORIENTED_EDGE('',*,*,#3068,.F.);
#4106=ORIENTED_EDGE('',*,*,#3064,.F.);
#4107=ORIENTED_EDGE('',*,*,#3069,.T.);
#4108=ORIENTED_EDGE('',*,*,#2930,.F.);
#4109=ORIENTED_EDGE('',*,*,#3067,.T.);
#4110=ORIENTED_EDGE('',*,*,#3066,.F.);
#4111=ORIENTED_EDGE('',*,*,#3070,.F.);
#4112=ORIENTED_EDGE('',*,*,#2926,.F.);
#4113=ORIENTED_EDGE('',*,*,#3069,.F.);
#4114=ORIENTED_EDGE('',*,*,#2920,.F.);
#4115=ORIENTED_EDGE('',*,*,#3071,.T.);
#4116=ORIENTED_EDGE('',*,*,#2923,.F.);
#4117=ORIENTED_EDGE('',*,*,#3070,.T.);
#4118=ORIENTED_EDGE('',*,*,#2755,.T.);
#4119=ORIENTED_EDGE('',*,*,#2759,.T.);
#4120=ORIENTED_EDGE('',*,*,#2762,.T.);
#4121=ORIENTED_EDGE('',*,*,#2765,.T.);
#4122=ORIENTED_EDGE('',*,*,#2928,.F.);
#4123=ORIENTED_EDGE('',*,*,#3072,.T.);
#4124=ORIENTED_EDGE('',*,*,#3063,.F.);
#4125=ORIENTED_EDGE('',*,*,#3071,.F.);
#4126=ORIENTED_EDGE('',*,*,#2950,.F.);
#4127=ORIENTED_EDGE('',*,*,#2961,.F.);
#4128=ORIENTED_EDGE('',*,*,#2958,.F.);
#4129=ORIENTED_EDGE('',*,*,#3073,.F.);
#4130=ORIENTED_EDGE('',*,*,#2932,.F.);
#4131=ORIENTED_EDGE('',*,*,#3074,.T.);
#4132=ORIENTED_EDGE('',*,*,#2933,.F.);
#4133=ORIENTED_EDGE('',*,*,#3072,.F.);
#4134=ORIENTED_EDGE('',*,*,#3060,.F.);
#4135=ORIENTED_EDGE('',*,*,#3073,.T.);
#4136=ORIENTED_EDGE('',*,*,#3057,.F.);
#4137=ORIENTED_EDGE('',*,*,#3074,.F.);
#4138=ORIENTED_EDGE('',*,*,#2945,.F.);
#4139=ORIENTED_EDGE('',*,*,#2965,.F.);
#4140=ORIENTED_EDGE('',*,*,#3055,.F.);
#4141=ORIENTED_EDGE('',*,*,#3056,.F.);
#4142=ORIENTED_EDGE('',*,*,#2960,.F.);
#4143=ORIENTED_EDGE('',*,*,#3053,.F.);
#4144=ORIENTED_EDGE('',*,*,#3051,.F.);
#4145=ORIENTED_EDGE('',*,*,#3049,.F.);
#4146=ORIENTED_EDGE('',*,*,#2978,.F.);
#4147=ORIENTED_EDGE('',*,*,#3052,.F.);
#4148=ORIENTED_EDGE('',*,*,#3054,.F.);
#4149=ORIENTED_EDGE('',*,*,#2980,.F.);
#4150=ORIENTED_EDGE('',*,*,#2979,.F.);
#4151=ORIENTED_EDGE('',*,*,#2995,.F.);
#4152=ORIENTED_EDGE('',*,*,#3045,.F.);
#4153=ORIENTED_EDGE('',*,*,#3047,.F.);
#4154=ORIENTED_EDGE('',*,*,#2991,.F.);
#4155=ORIENTED_EDGE('',*,*,#3046,.F.);
#4156=ORIENTED_EDGE('',*,*,#3050,.F.);
#4157=ORIENTED_EDGE('',*,*,#3048,.F.);
#4158=ORIENTED_EDGE('',*,*,#2990,.F.);
#4159=ORIENTED_EDGE('',*,*,#2999,.F.);
#4160=ORIENTED_EDGE('',*,*,#3042,.F.);
#4161=ORIENTED_EDGE('',*,*,#3040,.F.);
#4162=ORIENTED_EDGE('',*,*,#3009,.F.);
#4163=ORIENTED_EDGE('',*,*,#3043,.F.);
#4164=ORIENTED_EDGE('',*,*,#3044,.F.);
#4165=ORIENTED_EDGE('',*,*,#3011,.F.);
#4166=ORIENTED_EDGE('',*,*,#3022,.F.);
#4167=ORIENTED_EDGE('',*,*,#3037,.F.);
#4168=ORIENTED_EDGE('',*,*,#3041,.F.);
#4169=ORIENTED_EDGE('',*,*,#3039,.F.);
#4170=ORIENTED_EDGE('',*,*,#3026,.F.);
#4171=ORIENTED_EDGE('',*,*,#3038,.F.);
#4172=ORIENTED_EDGE('',*,*,#3010,.F.);
#4173=ORIENTED_EDGE('',*,*,#3027,.F.);
#4174=ORIENTED_EDGE('',*,*,#3034,.F.);
#4175=ORIENTED_EDGE('',*,*,#3035,.F.);
#4176=ORIENTED_EDGE('',*,*,#3021,.F.);
#4177=ORIENTED_EDGE('',*,*,#3036,.F.);
#4178=ORIENTED_EDGE('',*,*,#3058,.F.);
#4179=ORIENTED_EDGE('',*,*,#3068,.T.);
#4180=ORIENTED_EDGE('',*,*,#2946,.F.);
#4181=ORIENTED_EDGE('',*,*,#2944,.F.);
#4182=ORIENTED_EDGE('',*,*,#2856,.F.);
#4183=ORIENTED_EDGE('',*,*,#2860,.F.);
#4184=ORIENTED_EDGE('',*,*,#2864,.F.);
#4185=ORIENTED_EDGE('',*,*,#2868,.F.);
#4186=ORIENTED_EDGE('',*,*,#2872,.F.);
#4187=ORIENTED_EDGE('',*,*,#2876,.F.);
#4188=ORIENTED_EDGE('',*,*,#2880,.F.);
#4189=ORIENTED_EDGE('',*,*,#2885,.F.);
#4190=ORIENTED_EDGE('',*,*,#2889,.F.);
#4191=ORIENTED_EDGE('',*,*,#2894,.F.);
#4192=ORIENTED_EDGE('',*,*,#2898,.F.);
#4193=ORIENTED_EDGE('',*,*,#2902,.F.);
#4194=ORIENTED_EDGE('',*,*,#2906,.F.);
#4195=ORIENTED_EDGE('',*,*,#2910,.F.);
#4196=ORIENTED_EDGE('',*,*,#2914,.F.);
#4197=ORIENTED_EDGE('',*,*,#2918,.F.);
#5152=CYLINDRICAL_SURFACE('',#5836,5.13675);
#5153=CYLINDRICAL_SURFACE('',#5855,5.);
#5154=CYLINDRICAL_SURFACE('',#5862,5.);
#5155=CYLINDRICAL_SURFACE('',#5896,1.5);
#5156=CYLINDRICAL_SURFACE('',#5901,1.5);
#5157=CYLINDRICAL_SURFACE('',#5906,1.5);
#5158=CYLINDRICAL_SURFACE('',#5911,1.5);
#5159=CYLINDRICAL_SURFACE('',#5916,1.5);
#5160=CYLINDRICAL_SURFACE('',#5921,1.5);
#5161=CYLINDRICAL_SURFACE('',#5926,1.5);
#5162=CYLINDRICAL_SURFACE('',#5932,1.5);
#5163=CYLINDRICAL_SURFACE('',#5937,1.5);
#5164=CYLINDRICAL_SURFACE('',#5943,1.5);
#5165=CYLINDRICAL_SURFACE('',#5948,1.5);
#5166=CYLINDRICAL_SURFACE('',#5953,1.5);
#5167=CYLINDRICAL_SURFACE('',#5958,1.5);
#5168=CYLINDRICAL_SURFACE('',#5963,1.5);
#5169=CYLINDRICAL_SURFACE('',#5968,1.5);
#5170=CYLINDRICAL_SURFACE('',#5973,1.5);
#5171=CYLINDRICAL_SURFACE('',#5975,0.3);
#5172=CYLINDRICAL_SURFACE('',#5978,0.3);
#5173=CYLINDRICAL_SURFACE('',#5981,0.3);
#5174=CYLINDRICAL_SURFACE('',#5983,0.3);
#5175=CYLINDRICAL_SURFACE('',#5985,0.3);
#5176=CYLINDRICAL_SURFACE('',#5987,0.3);
#5177=CYLINDRICAL_SURFACE('',#5989,0.3);
#5178=CYLINDRICAL_SURFACE('',#5992,0.3);
#5179=CYLINDRICAL_SURFACE('',#6002,0.3);
#5180=CYLINDRICAL_SURFACE('',#6003,0.3);
#5181=CYLINDRICAL_SURFACE('',#6008,0.3);
#5182=CYLINDRICAL_SURFACE('',#6018,0.3);
#5183=CYLINDRICAL_SURFACE('',#6020,0.3);
#5184=CYLINDRICAL_SURFACE('',#6025,0.3);
#5185=CYLINDRICAL_SURFACE('',#6042,0.3);
#5186=CYLINDRICAL_SURFACE('',#6043,0.3);
#5187=CYLINDRICAL_SURFACE('',#6056,0.3);
#5188=CYLINDRICAL_SURFACE('',#6061,0.3);
#5189=CYLINDRICAL_SURFACE('',#6066,0.3);
#5190=CYLINDRICAL_SURFACE('',#6079,0.3);
#5191=CYLINDRICAL_SURFACE('',#6080,0.3);
#5192=CYLINDRICAL_SURFACE('',#6093,0.3);
#5193=CYLINDRICAL_SURFACE('',#6098,0.3);
#5194=CYLINDRICAL_SURFACE('',#6099,0.3);
#5195=CYLINDRICAL_SURFACE('',#6108,0.3);
#5196=CYLINDRICAL_SURFACE('',#6109,0.3);
#5197=CYLINDRICAL_SURFACE('',#6110,0.3);
#5198=CYLINDRICAL_SURFACE('',#6111,0.3);
#5199=CYLINDRICAL_SURFACE('',#6112,0.3);
#5200=CYLINDRICAL_SURFACE('',#6113,0.3);
#5201=CYLINDRICAL_SURFACE('',#6114,0.3);
#5202=CYLINDRICAL_SURFACE('',#6115,0.3);
#5203=CYLINDRICAL_SURFACE('',#6116,0.3);
#5204=CYLINDRICAL_SURFACE('',#6117,0.3);
#5205=CYLINDRICAL_SURFACE('',#6118,0.3);
#5206=CYLINDRICAL_SURFACE('',#6119,0.3);
#5207=CYLINDRICAL_SURFACE('',#6120,0.3);
#5208=CYLINDRICAL_SURFACE('',#6121,0.3);
#5209=CYLINDRICAL_SURFACE('',#6122,0.3);
#5210=CYLINDRICAL_SURFACE('',#6123,0.3);
#5211=CYLINDRICAL_SURFACE('',#6124,0.3);
#5212=CYLINDRICAL_SURFACE('',#6125,0.3);
#5213=CYLINDRICAL_SURFACE('',#6126,0.3);
#5214=CYLINDRICAL_SURFACE('',#6127,0.3);
#5215=CYLINDRICAL_SURFACE('',#6128,0.3);
#5216=CYLINDRICAL_SURFACE('',#6129,0.3);
#5217=CYLINDRICAL_SURFACE('',#6130,0.3);
#5218=CYLINDRICAL_SURFACE('',#6132,0.3);
#5219=CYLINDRICAL_SURFACE('',#6133,0.3);
#5220=CYLINDRICAL_SURFACE('',#6135,0.3);
#5221=CYLINDRICAL_SURFACE('',#6136,0.3);
#5222=CYLINDRICAL_SURFACE('',#6138,0.3);
#5326=ADVANCED_FACE('',(#383),#5152,.F.);
#5327=ADVANCED_FACE('',(#384),#294,.T.);
#5328=ADVANCED_FACE('',(#385,#247),#295,.T.);
#5329=ADVANCED_FACE('',(#386),#296,.T.);
#5330=ADVANCED_FACE('',(#387,#248),#297,.T.);
#5331=ADVANCED_FACE('',(#388),#298,.T.);
#5332=ADVANCED_FACE('',(#389),#179,.T.);
#5333=ADVANCED_FACE('',(#390,#249,#250),#299,.T.);
#5334=ADVANCED_FACE('',(#391),#5153,.F.);
#5335=ADVANCED_FACE('',(#392),#180,.T.);
#5336=ADVANCED_FACE('',(#393),#5154,.F.);
#5337=ADVANCED_FACE('',(#394),#181,.T.);
#5338=ADVANCED_FACE('',(#395,#251,#252),#300,.T.);
#5339=ADVANCED_FACE('',(#396),#182,.T.);
#5340=ADVANCED_FACE('',(#397),#183,.T.);
#5341=ADVANCED_FACE('',(#398,#253,#254,#255,#256,#257,#258,#259,#260,#261,
#262,#263,#264,#265,#266,#267,#268),#301,.T.);
#5342=ADVANCED_FACE('',(#399),#5155,.F.);
#5343=ADVANCED_FACE('',(#400),#184,.T.);
#5344=ADVANCED_FACE('',(#401),#5156,.F.);
#5345=ADVANCED_FACE('',(#402),#185,.T.);
#5346=ADVANCED_FACE('',(#403),#5157,.F.);
#5347=ADVANCED_FACE('',(#404),#186,.T.);
#5348=ADVANCED_FACE('',(#405),#5158,.F.);
#5349=ADVANCED_FACE('',(#406),#187,.T.);
#5350=ADVANCED_FACE('',(#407),#5159,.F.);
#5351=ADVANCED_FACE('',(#408),#188,.T.);
#5352=ADVANCED_FACE('',(#409),#5160,.F.);
#5353=ADVANCED_FACE('',(#410),#189,.T.);
#5354=ADVANCED_FACE('',(#411),#5161,.F.);
#5355=ADVANCED_FACE('',(#412),#190,.T.);
#5356=ADVANCED_FACE('',(#413),#5162,.F.);
#5357=ADVANCED_FACE('',(#414),#191,.T.);
#5358=ADVANCED_FACE('',(#415),#5163,.F.);
#5359=ADVANCED_FACE('',(#416),#192,.T.);
#5360=ADVANCED_FACE('',(#417),#5164,.F.);
#5361=ADVANCED_FACE('',(#418),#193,.T.);
#5362=ADVANCED_FACE('',(#419),#5165,.F.);
#5363=ADVANCED_FACE('',(#420),#194,.T.);
#5364=ADVANCED_FACE('',(#421),#5166,.F.);
#5365=ADVANCED_FACE('',(#422),#195,.T.);
#5366=ADVANCED_FACE('',(#423),#5167,.F.);
#5367=ADVANCED_FACE('',(#424),#196,.T.);
#5368=ADVANCED_FACE('',(#425),#5168,.F.);
#5369=ADVANCED_FACE('',(#426),#197,.T.);
#5370=ADVANCED_FACE('',(#427),#5169,.F.);
#5371=ADVANCED_FACE('',(#428),#198,.T.);
#5372=ADVANCED_FACE('',(#429),#5170,.F.);
#5373=ADVANCED_FACE('',(#430),#5171,.T.);
#5374=ADVANCED_FACE('',(#431),#5172,.T.);
#5375=ADVANCED_FACE('',(#432),#5173,.T.);
#5376=ADVANCED_FACE('',(#433),#5174,.T.);
#5377=ADVANCED_FACE('',(#434),#5175,.T.);
#5378=ADVANCED_FACE('',(#435),#5176,.T.);
#5379=ADVANCED_FACE('',(#436),#5177,.T.);
#5380=ADVANCED_FACE('',(#437),#5178,.T.);
#5381=ADVANCED_FACE('',(#438),#107,.T.);
#5382=ADVANCED_FACE('',(#439),#108,.T.);
#5383=ADVANCED_FACE('',(#440),#5179,.T.);
#5384=ADVANCED_FACE('',(#441),#5180,.T.);
#5385=ADVANCED_FACE('',(#442),#109,.T.);
#5386=ADVANCED_FACE('',(#443),#5181,.T.);
#5387=ADVANCED_FACE('',(#444),#199,.T.);
#5388=ADVANCED_FACE('',(#445),#110,.T.);
#5389=ADVANCED_FACE('',(#446),#5182,.T.);
#5390=ADVANCED_FACE('',(#447),#5183,.T.);
#5391=ADVANCED_FACE('',(#448),#200,.T.);
#5392=ADVANCED_FACE('',(#449),#5184,.T.);
#5393=ADVANCED_FACE('',(#450),#201,.T.);
#5394=ADVANCED_FACE('',(#451),#111,.T.);
#5395=ADVANCED_FACE('',(#452),#202,.T.);
#5396=ADVANCED_FACE('',(#453),#112,.T.);
#5397=ADVANCED_FACE('',(#454),#5185,.T.);
#5398=ADVANCED_FACE('',(#455),#5186,.T.);
#5399=ADVANCED_FACE('',(#456),#113,.T.);
#5400=ADVANCED_FACE('',(#457),#203,.T.);
#5401=ADVANCED_FACE('',(#458),#114,.T.);
#5402=ADVANCED_FACE('',(#459),#5187,.T.);
#5403=ADVANCED_FACE('',(#460),#204,.T.);
#5404=ADVANCED_FACE('',(#461),#5188,.T.);
#5405=ADVANCED_FACE('',(#462),#205,.T.);
#5406=ADVANCED_FACE('',(#463),#5189,.T.);
#5407=ADVANCED_FACE('',(#464),#115,.T.);
#5408=ADVANCED_FACE('',(#465),#206,.T.);
#5409=ADVANCED_FACE('',(#466),#116,.T.);
#5410=ADVANCED_FACE('',(#467),#5190,.T.);
#5411=ADVANCED_FACE('',(#468),#5191,.T.);
#5412=ADVANCED_FACE('',(#469),#117,.T.);
#5413=ADVANCED_FACE('',(#470),#118,.T.);
#5414=ADVANCED_FACE('',(#471),#119,.T.);
#5415=ADVANCED_FACE('',(#472),#5192,.T.);
#5416=ADVANCED_FACE('',(#473),#120,.T.);
#5417=ADVANCED_FACE('',(#474),#5193,.T.);
#5418=ADVANCED_FACE('',(#475),#5194,.T.);
#5419=ADVANCED_FACE('',(#476),#121,.T.);
#5420=ADVANCED_FACE('',(#477),#122,.T.);
#5421=ADVANCED_FACE('',(#478),#5195,.T.);
#5422=ADVANCED_FACE('',(#479),#5196,.T.);
#5423=ADVANCED_FACE('',(#480),#5197,.T.);
#5424=ADVANCED_FACE('',(#481),#5198,.T.);
#5425=ADVANCED_FACE('',(#482),#5199,.T.);
#5426=ADVANCED_FACE('',(#483),#5200,.T.);
#5427=ADVANCED_FACE('',(#484),#5201,.T.);
#5428=ADVANCED_FACE('',(#485),#5202,.T.);
#5429=ADVANCED_FACE('',(#486),#5203,.T.);
#5430=ADVANCED_FACE('',(#487),#5204,.F.);
#5431=ADVANCED_FACE('',(#488),#5205,.T.);
#5432=ADVANCED_FACE('',(#489),#5206,.F.);
#5433=ADVANCED_FACE('',(#490),#5207,.T.);
#5434=ADVANCED_FACE('',(#491),#5208,.T.);
#5435=ADVANCED_FACE('',(#492),#5209,.T.);
#5436=ADVANCED_FACE('',(#493),#5210,.T.);
#5437=ADVANCED_FACE('',(#494),#5211,.F.);
#5438=ADVANCED_FACE('',(#495),#5212,.T.);
#5439=ADVANCED_FACE('',(#496),#5213,.T.);
#5440=ADVANCED_FACE('',(#497),#5214,.F.);
#5441=ADVANCED_FACE('',(#498),#5215,.T.);
#5442=ADVANCED_FACE('',(#499),#5216,.T.);
#5443=ADVANCED_FACE('',(#500),#5217,.T.);
#5444=ADVANCED_FACE('',(#501),#5218,.T.);
#5445=ADVANCED_FACE('',(#502),#5219,.T.);
#5446=ADVANCED_FACE('',(#503),#5220,.T.);
#5447=ADVANCED_FACE('',(#504),#5221,.T.);
#5448=ADVANCED_FACE('',(#505),#5222,.T.);
#5449=ADVANCED_FACE('',(#506),#302,.T.);
#5450=ADVANCED_FACE('',(#507),#303,.T.);
#5451=ADVANCED_FACE('',(#508),#304,.T.);
#5452=ADVANCED_FACE('',(#509,#269),#305,.T.);
#5453=ADVANCED_FACE('',(#510),#306,.F.);
#5454=ADVANCED_FACE('',(#511),#307,.F.);
#5455=ADVANCED_FACE('',(#512),#308,.F.);
#5456=ADVANCED_FACE('',(#513),#309,.F.);
#5457=ADVANCED_FACE('',(#514),#310,.T.);
#5458=ADVANCED_FACE('',(#515),#311,.F.);
#5459=ADVANCED_FACE('',(#516),#312,.T.);
#5460=ADVANCED_FACE('',(#517),#313,.T.);
#5461=ADVANCED_FACE('',(#518),#314,.F.);
#5462=ADVANCED_FACE('',(#519),#315,.F.);
#5463=ADVANCED_FACE('',(#520),#316,.T.);
#5464=ADVANCED_FACE('',(#521),#317,.T.);
#5465=ADVANCED_FACE('',(#522),#318,.T.);
#5466=ADVANCED_FACE('',(#523),#319,.T.);
#5467=ADVANCED_FACE('',(#524),#320,.T.);
#5468=ADVANCED_FACE('',(#525),#321,.T.);
#5469=ADVANCED_FACE('',(#526),#322,.T.);
#5470=ADVANCED_FACE('',(#527),#323,.T.);
#5471=ADVANCED_FACE('',(#528),#324,.T.);
#5472=ADVANCED_FACE('',(#529),#325,.T.);
#5473=ADVANCED_FACE('',(#530),#326,.T.);
#5474=ADVANCED_FACE('',(#531),#327,.T.);
#5475=ADVANCED_FACE('',(#532),#328,.T.);
#5476=ADVANCED_FACE('',(#533),#329,.T.);
#5477=ADVANCED_FACE('',(#534),#330,.T.);
#5478=ADVANCED_FACE('',(#535),#331,.T.);
#5479=ADVANCED_FACE('',(#536),#332,.T.);
#5480=ADVANCED_FACE('',(#537),#333,.T.);
#5481=ADVANCED_FACE('',(#538),#334,.T.);
#5482=ADVANCED_FACE('',(#539),#335,.T.);
#5483=ADVANCED_FACE('',(#540),#336,.T.);
#5713=CLOSED_SHELL('',(#5326,#5327,#5328,#5329,#5330,#5331,#5332,#5333,
#5334,#5335,#5336,#5337,#5338,#5339,#5340,#5341,#5342,#5343,#5344,#5345,
#5346,#5347,#5348,#5349,#5350,#5351,#5352,#5353,#5354,#5355,#5356,#5357,
#5358,#5359,#5360,#5361,#5362,#5363,#5364,#5365,#5366,#5367,#5368,#5369,
#5370,#5371,#5372,#5373,#5374,#5375,#5376,#5377,#5378,#5379,#5380,#5381,
#5382,#5383,#5384,#5385,#5386,#5387,#5388,#5389,#5390,#5391,#5392,#5393,
#5394,#5395,#5396,#5397,#5398,#5399,#5400,#5401,#5402,#5403,#5404,#5405,
#5406,#5407,#5408,#5409,#5410,#5411,#5412,#5413,#5414,#5415,#5416,#5417,
#5418,#5419,#5420,#5421,#5422,#5423,#5424,#5425,#5426,#5427,#5428,#5429,
#5430,#5431,#5432,#5433,#5434,#5435,#5436,#5437,#5438,#5439,#5440,#5441,
#5442,#5443,#5444,#5445,#5446,#5447,#5448,#5449,#5450,#5451,#5452,#5453,
#5454,#5455,#5456,#5457,#5458,#5459,#5460,#5461,#5462,#5463,#5464,#5465,
#5466,#5467,#5468,#5469,#5470,#5471,#5472,#5473,#5474,#5475,#5476,#5477,
#5478,#5479,#5480,#5481,#5482,#5483));
#5835=AXIS2_PLACEMENT_3D('',#8751,#6698,#6699);
#5836=AXIS2_PLACEMENT_3D('',#8752,#6700,#6701);
#5837=AXIS2_PLACEMENT_3D('',#8754,#6702,#6703);
#5838=AXIS2_PLACEMENT_3D('',#8757,#6705,#6706);
#5839=AXIS2_PLACEMENT_3D('',#8758,#6707,#6708);
#5840=AXIS2_PLACEMENT_3D('',#8767,#6713,#6714);
#5841=AXIS2_PLACEMENT_3D('',#8773,#6718,#6719);
#5842=AXIS2_PLACEMENT_3D('',#8779,#6723,#6724);
#5843=AXIS2_PLACEMENT_3D('',#8782,#6727,#6728);
#5844=AXIS2_PLACEMENT_3D('',#8783,#6729,#6730);
#5845=AXIS2_PLACEMENT_3D('',#8785,#6731,#6732);
#5846=AXIS2_PLACEMENT_3D('',#8787,#6733,#6734);
#5847=AXIS2_PLACEMENT_3D('',#8789,#6735,#6736);
#5848=AXIS2_PLACEMENT_3D('',#8790,#6737,#6738);
#5849=AXIS2_PLACEMENT_3D('',#8791,#6739,#6740);
#5850=AXIS2_PLACEMENT_3D('',#8798,#6743,#6744);
#5851=AXIS2_PLACEMENT_3D('',#8804,#6747,#6748);
#5852=AXIS2_PLACEMENT_3D('',#8828,#6760,#6761);
#5853=AXIS2_PLACEMENT_3D('',#8834,#6764,#6765);
#5854=AXIS2_PLACEMENT_3D('',#8841,#6769,#6770);
#5855=AXIS2_PLACEMENT_3D('',#8842,#6771,#6772);
#5856=AXIS2_PLACEMENT_3D('',#8846,#6774,#6775);
#5857=AXIS2_PLACEMENT_3D('',#8847,#6776,#6777);
#5858=AXIS2_PLACEMENT_3D('',#8848,#6778,#6779);
#5859=AXIS2_PLACEMENT_3D('',#8851,#6780,#6781);
#5860=AXIS2_PLACEMENT_3D('',#8852,#6782,#6783);
#5861=AXIS2_PLACEMENT_3D('',#8853,#6784,#6785);
#5862=AXIS2_PLACEMENT_3D('',#8854,#6786,#6787);
#5863=AXIS2_PLACEMENT_3D('',#8858,#6789,#6790);
#5864=AXIS2_PLACEMENT_3D('',#8859,#6791,#6792);
#5865=AXIS2_PLACEMENT_3D('',#8860,#6793,#6794);
#5866=AXIS2_PLACEMENT_3D('',#8862,#6795,#6796);
#5867=AXIS2_PLACEMENT_3D('',#8863,#6797,#6798);
#5868=AXIS2_PLACEMENT_3D('',#8864,#6799,#6800);
#5869=AXIS2_PLACEMENT_3D('',#8867,#6801,#6802);
#5870=AXIS2_PLACEMENT_3D('',#8879,#6808,#6809);
#5871=AXIS2_PLACEMENT_3D('',#8885,#6812,#6813);
#5872=AXIS2_PLACEMENT_3D('',#8909,#6825,#6826);
#5873=AXIS2_PLACEMENT_3D('',#8914,#6829,#6830);
#5874=AXIS2_PLACEMENT_3D('',#8915,#6831,#6832);
#5875=AXIS2_PLACEMENT_3D('',#8916,#6833,#6834);
#5876=AXIS2_PLACEMENT_3D('',#8917,#6835,#6836);
#5877=AXIS2_PLACEMENT_3D('',#8919,#6837,#6838);
#5878=AXIS2_PLACEMENT_3D('',#8921,#6839,#6840);
#5879=AXIS2_PLACEMENT_3D('',#8922,#6841,#6842);
#5880=AXIS2_PLACEMENT_3D('',#8923,#6843,#6844);
#5881=AXIS2_PLACEMENT_3D('',#8933,#6849,#6850);
#5882=AXIS2_PLACEMENT_3D('',#8935,#6851,#6852);
#5883=AXIS2_PLACEMENT_3D('',#8937,#6853,#6854);
#5884=AXIS2_PLACEMENT_3D('',#8939,#6855,#6856);
#5885=AXIS2_PLACEMENT_3D('',#8941,#6857,#6858);
#5886=AXIS2_PLACEMENT_3D('',#8943,#6859,#6860);
#5887=AXIS2_PLACEMENT_3D('',#8945,#6861,#6862);
#5888=AXIS2_PLACEMENT_3D('',#8947,#6863,#6864);
#5889=AXIS2_PLACEMENT_3D('',#8949,#6865,#6866);
#5890=AXIS2_PLACEMENT_3D('',#8951,#6867,#6868);
#5891=AXIS2_PLACEMENT_3D('',#8953,#6869,#6870);
#5892=AXIS2_PLACEMENT_3D('',#8955,#6871,#6872);
#5893=AXIS2_PLACEMENT_3D('',#8957,#6873,#6874);
#5894=AXIS2_PLACEMENT_3D('',#8959,#6875,#6876);
#5895=AXIS2_PLACEMENT_3D('',#8961,#6877,#6878);
#5896=AXIS2_PLACEMENT_3D('',#8962,#6879,#6880);
#5897=AXIS2_PLACEMENT_3D('',#8965,#6882,#6883);
#5898=AXIS2_PLACEMENT_3D('',#8966,#6884,#6885);
#5899=AXIS2_PLACEMENT_3D('',#8968,#6886,#6887);
#5900=AXIS2_PLACEMENT_3D('',#8969,#6888,#6889);
#5901=AXIS2_PLACEMENT_3D('',#8970,#6890,#6891);
#5902=AXIS2_PLACEMENT_3D('',#8973,#6893,#6894);
#5903=AXIS2_PLACEMENT_3D('',#8974,#6895,#6896);
#5904=AXIS2_PLACEMENT_3D('',#8976,#6897,#6898);
#5905=AXIS2_PLACEMENT_3D('',#8977,#6899,#6900);
#5906=AXIS2_PLACEMENT_3D('',#8978,#6901,#6902);
#5907=AXIS2_PLACEMENT_3D('',#8981,#6904,#6905);
#5908=AXIS2_PLACEMENT_3D('',#8982,#6906,#6907);
#5909=AXIS2_PLACEMENT_3D('',#8984,#6908,#6909);
#5910=AXIS2_PLACEMENT_3D('',#8985,#6910,#6911);
#5911=AXIS2_PLACEMENT_3D('',#8986,#6912,#6913);
#5912=AXIS2_PLACEMENT_3D('',#8989,#6915,#6916);
#5913=AXIS2_PLACEMENT_3D('',#8990,#6917,#6918);
#5914=AXIS2_PLACEMENT_3D('',#8992,#6919,#6920);
#5915=AXIS2_PLACEMENT_3D('',#8993,#6921,#6922);
#5916=AXIS2_PLACEMENT_3D('',#8994,#6923,#6924);
#5917=AXIS2_PLACEMENT_3D('',#8997,#6926,#6927);
#5918=AXIS2_PLACEMENT_3D('',#8998,#6928,#6929);
#5919=AXIS2_PLACEMENT_3D('',#9000,#6930,#6931);
#5920=AXIS2_PLACEMENT_3D('',#9001,#6932,#6933);
#5921=AXIS2_PLACEMENT_3D('',#9002,#6934,#6935);
#5922=AXIS2_PLACEMENT_3D('',#9005,#6937,#6938);
#5923=AXIS2_PLACEMENT_3D('',#9006,#6939,#6940);
#5924=AXIS2_PLACEMENT_3D('',#9008,#6941,#6942);
#5925=AXIS2_PLACEMENT_3D('',#9009,#6943,#6944);
#5926=AXIS2_PLACEMENT_3D('',#9010,#6945,#6946);
#5927=AXIS2_PLACEMENT_3D('',#9013,#6948,#6949);
#5928=AXIS2_PLACEMENT_3D('',#9014,#6950,#6951);
#5929=AXIS2_PLACEMENT_3D('',#9016,#6952,#6953);
#5930=AXIS2_PLACEMENT_3D('',#9018,#6954,#6955);
#5931=AXIS2_PLACEMENT_3D('',#9019,#6956,#6957);
#5932=AXIS2_PLACEMENT_3D('',#9020,#6958,#6959);
#5933=AXIS2_PLACEMENT_3D('',#9023,#6961,#6962);
#5934=AXIS2_PLACEMENT_3D('',#9024,#6963,#6964);
#5935=AXIS2_PLACEMENT_3D('',#9026,#6965,#6966);
#5936=AXIS2_PLACEMENT_3D('',#9027,#6967,#6968);
#5937=AXIS2_PLACEMENT_3D('',#9028,#6969,#6970);
#5938=AXIS2_PLACEMENT_3D('',#9031,#6972,#6973);
#5939=AXIS2_PLACEMENT_3D('',#9032,#6974,#6975);
#5940=AXIS2_PLACEMENT_3D('',#9034,#6976,#6977);
#5941=AXIS2_PLACEMENT_3D('',#9036,#6978,#6979);
#5942=AXIS2_PLACEMENT_3D('',#9037,#6980,#6981);
#5943=AXIS2_PLACEMENT_3D('',#9038,#6982,#6983);
#5944=AXIS2_PLACEMENT_3D('',#9041,#6985,#6986);
#5945=AXIS2_PLACEMENT_3D('',#9042,#6987,#6988);
#5946=AXIS2_PLACEMENT_3D('',#9044,#6989,#6990);
#5947=AXIS2_PLACEMENT_3D('',#9045,#6991,#6992);
#5948=AXIS2_PLACEMENT_3D('',#9046,#6993,#6994);
#5949=AXIS2_PLACEMENT_3D('',#9049,#6996,#6997);
#5950=AXIS2_PLACEMENT_3D('',#9050,#6998,#6999);
#5951=AXIS2_PLACEMENT_3D('',#9052,#7000,#7001);
#5952=AXIS2_PLACEMENT_3D('',#9053,#7002,#7003);
#5953=AXIS2_PLACEMENT_3D('',#9054,#7004,#7005);
#5954=AXIS2_PLACEMENT_3D('',#9057,#7007,#7008);
#5955=AXIS2_PLACEMENT_3D('',#9058,#7009,#7010);
#5956=AXIS2_PLACEMENT_3D('',#9060,#7011,#7012);
#5957=AXIS2_PLACEMENT_3D('',#9061,#7013,#7014);
#5958=AXIS2_PLACEMENT_3D('',#9062,#7015,#7016);
#5959=AXIS2_PLACEMENT_3D('',#9065,#7018,#7019);
#5960=AXIS2_PLACEMENT_3D('',#9066,#7020,#7021);
#5961=AXIS2_PLACEMENT_3D('',#9068,#7022,#7023);
#5962=AXIS2_PLACEMENT_3D('',#9069,#7024,#7025);
#5963=AXIS2_PLACEMENT_3D('',#9070,#7026,#7027);
#5964=AXIS2_PLACEMENT_3D('',#9073,#7029,#7030);
#5965=AXIS2_PLACEMENT_3D('',#9074,#7031,#7032);
#5966=AXIS2_PLACEMENT_3D('',#9076,#7033,#7034);
#5967=AXIS2_PLACEMENT_3D('',#9077,#7035,#7036);
#5968=AXIS2_PLACEMENT_3D('',#9078,#7037,#7038);
#5969=AXIS2_PLACEMENT_3D('',#9081,#7040,#7041);
#5970=AXIS2_PLACEMENT_3D('',#9082,#7042,#7043);
#5971=AXIS2_PLACEMENT_3D('',#9084,#7044,#7045);
#5972=AXIS2_PLACEMENT_3D('',#9085,#7046,#7047);
#5973=AXIS2_PLACEMENT_3D('',#9086,#7048,#7049);
#5974=AXIS2_PLACEMENT_3D('',#9089,#7051,#7052);
#5975=AXIS2_PLACEMENT_3D('',#9090,#7053,#7054);
#5976=AXIS2_PLACEMENT_3D('',#9092,#7055,#7056);
#5977=AXIS2_PLACEMENT_3D('',#9095,#7058,#7059);
#5978=AXIS2_PLACEMENT_3D('',#9096,#7060,#7061);
#5979=AXIS2_PLACEMENT_3D('',#9098,#7062,#7063);
#5980=AXIS2_PLACEMENT_3D('',#9101,#7065,#7066);
#5981=AXIS2_PLACEMENT_3D('',#9102,#7067,#7068);
#5982=AXIS2_PLACEMENT_3D('',#9104,#7069,#7070);
#5983=AXIS2_PLACEMENT_3D('',#9106,#7072,#7073);
#5984=AXIS2_PLACEMENT_3D('',#9108,#7074,#7075);
#5985=AXIS2_PLACEMENT_3D('',#9110,#7077,#7078);
#5986=AXIS2_PLACEMENT_3D('',#9112,#7079,#7080);
#5987=AXIS2_PLACEMENT_3D('',#9114,#7082,#7083);
#5988=AXIS2_PLACEMENT_3D('',#9116,#7084,#7085);
#5989=AXIS2_PLACEMENT_3D('',#9118,#7087,#7088);
#5990=AXIS2_PLACEMENT_3D('',#9122,#7090,#7091);
#5991=AXIS2_PLACEMENT_3D('',#9123,#7092,#7093);
#5992=AXIS2_PLACEMENT_3D('',#9124,#7094,#7095);
#5993=AXIS2_PLACEMENT_3D('',#9126,#7096,#7097);
#5994=AXIS2_PLACEMENT_3D('',#9128,#7099,#7100);
#5995=AXIS2_PLACEMENT_3D('',#9130,#7101,#7102);
#5996=AXIS2_PLACEMENT_3D('',#9132,#7103,#7104);
#5997=AXIS2_PLACEMENT_3D('',#9133,#7105,#7106);
#5998=AXIS2_PLACEMENT_3D('',#9134,#7107,#7108);
#5999=AXIS2_PLACEMENT_3D('',#9136,#7109,#7110);
#6000=AXIS2_PLACEMENT_3D('',#9138,#7111,#7112);
#6001=AXIS2_PLACEMENT_3D('',#9139,#7113,#7114);
#6002=AXIS2_PLACEMENT_3D('',#9140,#7115,#7116);
#6003=AXIS2_PLACEMENT_3D('',#9143,#7119,#7120);
#6004=AXIS2_PLACEMENT_3D('',#9145,#7122,#7123);
#6005=AXIS2_PLACEMENT_3D('',#9148,#7124,#7125);
#6006=AXIS2_PLACEMENT_3D('',#9149,#7126,#7127);
#6007=AXIS2_PLACEMENT_3D('',#9150,#7128,#7129);
#6008=AXIS2_PLACEMENT_3D('',#9151,#7130,#7131);
#6009=AXIS2_PLACEMENT_3D('',#9154,#7133,#7134);
#6010=AXIS2_PLACEMENT_3D('',#9155,#7135,#7136);
#6011=AXIS2_PLACEMENT_3D('',#9158,#7137,#7138);
#6012=AXIS2_PLACEMENT_3D('',#9159,#7139,#7140);
#6013=AXIS2_PLACEMENT_3D('',#9160,#7141,#7142);
#6014=AXIS2_PLACEMENT_3D('',#9161,#7143,#7144);
#6015=AXIS2_PLACEMENT_3D('',#9163,#7145,#7146);
#6016=AXIS2_PLACEMENT_3D('',#9165,#7147,#7148);
#6017=AXIS2_PLACEMENT_3D('',#9166,#7149,#7150);
#6018=AXIS2_PLACEMENT_3D('',#9167,#7151,#7152);
#6019=AXIS2_PLACEMENT_3D('',#9170,#7154,#7155);
#6020=AXIS2_PLACEMENT_3D('',#9171,#7156,#7157);
#6021=AXIS2_PLACEMENT_3D('',#9174,#7160,#7161);
#6022=AXIS2_PLACEMENT_3D('',#9177,#7162,#7163);
#6023=AXIS2_PLACEMENT_3D('',#9178,#7164,#7165);
#6024=AXIS2_PLACEMENT_3D('',#9179,#7166,#7167);
#6025=AXIS2_PLACEMENT_3D('',#9180,#7168,#7169);
#6026=AXIS2_PLACEMENT_3D('',#9182,#7171,#7172);
#6027=AXIS2_PLACEMENT_3D('',#9184,#7173,#7174);
#6028=AXIS2_PLACEMENT_3D('',#9186,#7175,#7176);
#6029=AXIS2_PLACEMENT_3D('',#9187,#7177,#7178);
#6030=AXIS2_PLACEMENT_3D('',#9188,#7179,#7180);
#6031=AXIS2_PLACEMENT_3D('',#9190,#7181,#7182);
#6032=AXIS2_PLACEMENT_3D('',#9192,#7183,#7184);
#6033=AXIS2_PLACEMENT_3D('',#9193,#7185,#7186);
#6034=AXIS2_PLACEMENT_3D('',#9194,#7187,#7188);
#6035=AXIS2_PLACEMENT_3D('',#9197,#7189,#7190);
#6036=AXIS2_PLACEMENT_3D('',#9198,#7191,#7192);
#6037=AXIS2_PLACEMENT_3D('',#9199,#7193,#7194);
#6038=AXIS2_PLACEMENT_3D('',#9200,#7195,#7196);
#6039=AXIS2_PLACEMENT_3D('',#9202,#7197,#7198);
#6040=AXIS2_PLACEMENT_3D('',#9204,#7199,#7200);
#6041=AXIS2_PLACEMENT_3D('',#9205,#7201,#7202);
#6042=AXIS2_PLACEMENT_3D('',#9206,#7203,#7204);
#6043=AXIS2_PLACEMENT_3D('',#9209,#7207,#7208);
#6044=AXIS2_PLACEMENT_3D('',#9211,#7210,#7211);
#6045=AXIS2_PLACEMENT_3D('',#9213,#7212,#7213);
#6046=AXIS2_PLACEMENT_3D('',#9215,#7214,#7215);
#6047=AXIS2_PLACEMENT_3D('',#9216,#7216,#7217);
#6048=AXIS2_PLACEMENT_3D('',#9217,#7218,#7219);
#6049=AXIS2_PLACEMENT_3D('',#9220,#7220,#7221);
#6050=AXIS2_PLACEMENT_3D('',#9221,#7222,#7223);
#6051=AXIS2_PLACEMENT_3D('',#9222,#7224,#7225);
#6052=AXIS2_PLACEMENT_3D('',#9223,#7226,#7227);
#6053=AXIS2_PLACEMENT_3D('',#9225,#7228,#7229);
#6054=AXIS2_PLACEMENT_3D('',#9227,#7230,#7231);
#6055=AXIS2_PLACEMENT_3D('',#9228,#7232,#7233);
#6056=AXIS2_PLACEMENT_3D('',#9229,#7234,#7235);
#6057=AXIS2_PLACEMENT_3D('',#9232,#7238,#7239);
#6058=AXIS2_PLACEMENT_3D('',#9235,#7240,#7241);
#6059=AXIS2_PLACEMENT_3D('',#9236,#7242,#7243);
#6060=AXIS2_PLACEMENT_3D('',#9237,#7244,#7245);
#6061=AXIS2_PLACEMENT_3D('',#9238,#7246,#7247);
#6062=AXIS2_PLACEMENT_3D('',#9240,#7249,#7250);
#6063=AXIS2_PLACEMENT_3D('',#9243,#7251,#7252);
#6064=AXIS2_PLACEMENT_3D('',#9244,#7253,#7254);
#6065=AXIS2_PLACEMENT_3D('',#9245,#7255,#7256);
#6066=AXIS2_PLACEMENT_3D('',#9246,#7257,#7258);
#6067=AXIS2_PLACEMENT_3D('',#9248,#7260,#7261);
#6068=AXIS2_PLACEMENT_3D('',#9250,#7262,#7263);
#6069=AXIS2_PLACEMENT_3D('',#9252,#7264,#7265);
#6070=AXIS2_PLACEMENT_3D('',#9253,#7266,#7267);
#6071=AXIS2_PLACEMENT_3D('',#9254,#7268,#7269);
#6072=AXIS2_PLACEMENT_3D('',#9257,#7270,#7271);
#6073=AXIS2_PLACEMENT_3D('',#9258,#7272,#7273);
#6074=AXIS2_PLACEMENT_3D('',#9259,#7274,#7275);
#6075=AXIS2_PLACEMENT_3D('',#9260,#7276,#7277);
#6076=AXIS2_PLACEMENT_3D('',#9262,#7278,#7279);
#6077=AXIS2_PLACEMENT_3D('',#9264,#7280,#7281);
#6078=AXIS2_PLACEMENT_3D('',#9265,#7282,#7283);
#6079=AXIS2_PLACEMENT_3D('',#9266,#7284,#7285);
#6080=AXIS2_PLACEMENT_3D('',#9269,#7288,#7289);
#6081=AXIS2_PLACEMENT_3D('',#9271,#7291,#7292);
#6082=AXIS2_PLACEMENT_3D('',#9273,#7293,#7294);
#6083=AXIS2_PLACEMENT_3D('',#9275,#7295,#7296);
#6084=AXIS2_PLACEMENT_3D('',#9276,#7297,#7298);
#6085=AXIS2_PLACEMENT_3D('',#9277,#7299,#7300);
#6086=AXIS2_PLACEMENT_3D('',#9279,#7301,#7302);
#6087=AXIS2_PLACEMENT_3D('',#9280,#7303,#7304);
#6088=AXIS2_PLACEMENT_3D('',#9281,#7305,#7306);
#6089=AXIS2_PLACEMENT_3D('',#9282,#7307,#7308);
#6090=AXIS2_PLACEMENT_3D('',#9284,#7309,#7310);
#6091=AXIS2_PLACEMENT_3D('',#9286,#7311,#7312);
#6092=AXIS2_PLACEMENT_3D('',#9287,#7313,#7314);
#6093=AXIS2_PLACEMENT_3D('',#9288,#7315,#7316);
#6094=AXIS2_PLACEMENT_3D('',#9291,#7319,#7320);
#6095=AXIS2_PLACEMENT_3D('',#9292,#7321,#7322);
#6096=AXIS2_PLACEMENT_3D('',#9294,#7323,#7324);
#6097=AXIS2_PLACEMENT_3D('',#9295,#7325,#7326);
#6098=AXIS2_PLACEMENT_3D('',#9296,#7327,#7328);
#6099=AXIS2_PLACEMENT_3D('',#9298,#7330,#7331);
#6100=AXIS2_PLACEMENT_3D('',#9300,#7333,#7334);
#6101=AXIS2_PLACEMENT_3D('',#9301,#7335,#7336);
#6102=AXIS2_PLACEMENT_3D('',#9303,#7337,#7338);
#6103=AXIS2_PLACEMENT_3D('',#9304,#7339,#7340);
#6104=AXIS2_PLACEMENT_3D('',#9305,#7341,#7342);
#6105=AXIS2_PLACEMENT_3D('',#9307,#7343,#7344);
#6106=AXIS2_PLACEMENT_3D('',#9308,#7345,#7346);
#6107=AXIS2_PLACEMENT_3D('',#9309,#7347,#7348);
#6108=AXIS2_PLACEMENT_3D('',#9310,#7349,#7350);
#6109=AXIS2_PLACEMENT_3D('',#9312,#7352,#7353);
#6110=AXIS2_PLACEMENT_3D('',#9313,#7354,#7355);
#6111=AXIS2_PLACEMENT_3D('',#9315,#7357,#7358);
#6112=AXIS2_PLACEMENT_3D('',#9317,#7360,#7361);
#6113=AXIS2_PLACEMENT_3D('',#9318,#7362,#7363);
#6114=AXIS2_PLACEMENT_3D('',#9320,#7365,#7366);
#6115=AXIS2_PLACEMENT_3D('',#9322,#7368,#7369);
#6116=AXIS2_PLACEMENT_3D('',#9324,#7371,#7372);
#6117=AXIS2_PLACEMENT_3D('',#9326,#7374,#7375);
#6118=AXIS2_PLACEMENT_3D('',#9329,#7378,#7379);
#6119=AXIS2_PLACEMENT_3D('',#9331,#7381,#7382);
#6120=AXIS2_PLACEMENT_3D('',#9334,#7385,#7386);
#6121=AXIS2_PLACEMENT_3D('',#9336,#7388,#7389);
#6122=AXIS2_PLACEMENT_3D('',#9338,#7391,#7392);
#6123=AXIS2_PLACEMENT_3D('',#9340,#7394,#7395);
#6124=AXIS2_PLACEMENT_3D('',#9342,#7397,#7398);
#6125=AXIS2_PLACEMENT_3D('',#9345,#7401,#7402);
#6126=AXIS2_PLACEMENT_3D('',#9347,#7404,#7405);
#6127=AXIS2_PLACEMENT_3D('',#9349,#7407,#7408);
#6128=AXIS2_PLACEMENT_3D('',#9352,#7411,#7412);
#6129=AXIS2_PLACEMENT_3D('',#9354,#7414,#7415);
#6130=AXIS2_PLACEMENT_3D('',#9356,#7417,#7418);
#6131=AXIS2_PLACEMENT_3D('',#9359,#7420,#7421);
#6132=AXIS2_PLACEMENT_3D('',#9360,#7422,#7423);
#6133=AXIS2_PLACEMENT_3D('',#9362,#7425,#7426);
#6134=AXIS2_PLACEMENT_3D('',#9365,#7428,#7429);
#6135=AXIS2_PLACEMENT_3D('',#9366,#7430,#7431);
#6136=AXIS2_PLACEMENT_3D('',#9368,#7433,#7434);
#6137=AXIS2_PLACEMENT_3D('',#9371,#7436,#7437);
#6138=AXIS2_PLACEMENT_3D('',#9372,#7438,#7439);
#6139=AXIS2_PLACEMENT_3D('',#9374,#7441,#7442);
#6140=AXIS2_PLACEMENT_3D('',#9377,#7445,#7446);
#6141=AXIS2_PLACEMENT_3D('',#9379,#7448,#7449);
#6142=AXIS2_PLACEMENT_3D('',#9381,#7451,#7452);
#6143=AXIS2_PLACEMENT_3D('',#9383,#7454,#7455);
#6144=AXIS2_PLACEMENT_3D('',#9385,#7457,#7458);
#6145=AXIS2_PLACEMENT_3D('',#9387,#7460,#7461);
#6146=AXIS2_PLACEMENT_3D('',#9389,#7463,#7464);
#6147=AXIS2_PLACEMENT_3D('',#9390,#7465,#7466);
#6148=AXIS2_PLACEMENT_3D('',#9391,#7467,#7468);
#6149=AXIS2_PLACEMENT_3D('',#9392,#7469,#7470);
#6150=AXIS2_PLACEMENT_3D('',#9393,#7471,#7472);
#6151=AXIS2_PLACEMENT_3D('',#9394,#7473,#7474);
#6152=AXIS2_PLACEMENT_3D('',#9395,#7475,#7476);
#6153=AXIS2_PLACEMENT_3D('',#9396,#7477,#7478);
#6154=AXIS2_PLACEMENT_3D('',#9397,#7479,#7480);
#6155=AXIS2_PLACEMENT_3D('',#9398,#7481,#7482);
#6156=AXIS2_PLACEMENT_3D('',#9399,#7483,#7484);
#6157=AXIS2_PLACEMENT_3D('',#9400,#7485,#7486);
#6158=AXIS2_PLACEMENT_3D('',#9401,#7487,#7488);
#6159=AXIS2_PLACEMENT_3D('',#9402,#7489,#7490);
#6160=AXIS2_PLACEMENT_3D('',#9403,#7491,#7492);
#6161=AXIS2_PLACEMENT_3D('',#9404,#7493,#7494);
#6162=AXIS2_PLACEMENT_3D('',#9405,#7495,#7496);
#6163=AXIS2_PLACEMENT_3D('',#9406,#7497,#7498);
#6164=AXIS2_PLACEMENT_3D('',#9407,#7499,#7500);
#6165=AXIS2_PLACEMENT_3D('',#9408,#7501,#7502);
#6166=AXIS2_PLACEMENT_3D('',#9409,#7503,#7504);
#6167=AXIS2_PLACEMENT_3D('',#9410,#7505,#7506);
#6168=AXIS2_PLACEMENT_3D('',#9411,#7507,#7508);
#6169=AXIS2_PLACEMENT_3D('',#9412,#7509,#7510);
#6170=AXIS2_PLACEMENT_3D('',#9413,#7511,#7512);
#6171=AXIS2_PLACEMENT_3D('',#9414,#7513,#7514);
#6172=AXIS2_PLACEMENT_3D('',#9415,#7515,#7516);
#6173=AXIS2_PLACEMENT_3D('',#9416,#7517,#7518);
#6698=DIRECTION('axis',(0.,0.,1.));
#6699=DIRECTION('refdir',(1.,0.,0.));
#6700=DIRECTION('center_axis',(-1.,0.,0.));
#6701=DIRECTION('ref_axis',(0.,1.,0.));
#6702=DIRECTION('center_axis',(-1.,0.,0.));
#6703=DIRECTION('ref_axis',(0.,1.,0.));
#6704=DIRECTION('',(-1.,0.,0.));
#6705=DIRECTION('center_axis',(1.,0.,0.));
#6706=DIRECTION('ref_axis',(0.,1.,0.));
#6707=DIRECTION('center_axis',(0.,-1.,0.));
#6708=DIRECTION('ref_axis',(-1.,0.,0.));
#6709=DIRECTION('',(1.,0.,0.));
#6710=DIRECTION('',(0.,0.,-1.));
#6711=DIRECTION('',(-1.,0.,0.));
#6712=DIRECTION('',(0.,0.,-1.));
#6713=DIRECTION('center_axis',(1.,0.,0.));
#6714=DIRECTION('ref_axis',(0.,-1.,0.));
#6715=DIRECTION('',(0.,1.,0.));
#6716=DIRECTION('',(0.,-1.,0.));
#6717=DIRECTION('',(0.,0.,-1.));
#6718=DIRECTION('center_axis',(0.,1.,0.));
#6719=DIRECTION('ref_axis',(1.,0.,0.));
#6720=DIRECTION('',(-1.,0.,0.));
#6721=DIRECTION('',(1.,0.,0.));
#6722=DIRECTION('',(0.,0.,-1.));
#6723=DIRECTION('center_axis',(-1.,0.,0.));
#6724=DIRECTION('ref_axis',(0.,1.,0.));
#6725=DIRECTION('',(0.,-1.,0.));
#6726=DIRECTION('',(0.,1.,0.));
#6727=DIRECTION('center_axis',(0.,0.,-1.));
#6728=DIRECTION('ref_axis',(-1.,0.,0.));
#6729=DIRECTION('center_axis',(-1.,0.,0.));
#6730=DIRECTION('ref_axis',(0.,0.,1.));
#6731=DIRECTION('center_axis',(1.,0.,0.));
#6732=DIRECTION('ref_axis',(0.,1.,0.));
#6733=DIRECTION('center_axis',(0.,-1.,0.));
#6734=DIRECTION('ref_axis',(0.,0.,-1.));
#6735=DIRECTION('center_axis',(-1.,0.,0.));
#6736=DIRECTION('ref_axis',(0.,1.,0.));
#6737=DIRECTION('center_axis',(-1.,0.,0.));
#6738=DIRECTION('ref_axis',(0.,1.,0.));
#6739=DIRECTION('center_axis',(1.,0.,0.));
#6740=DIRECTION('ref_axis',(0.,0.,-1.));
#6741=DIRECTION('',(0.,0.,1.));
#6742=DIRECTION('',(0.,-1.,0.));
#6743=DIRECTION('center_axis',(1.,0.,0.));
#6744=DIRECTION('ref_axis',(0.,0.707106781186545,0.70710678118655));
#6745=DIRECTION('',(0.,0.,1.));
#6746=DIRECTION('',(0.,-1.,0.));
#6747=DIRECTION('center_axis',(1.,0.,0.));
#6748=DIRECTION('ref_axis',(0.,0.707106781186545,0.70710678118655));
#6749=DIRECTION('',(0.,0.,1.));
#6750=DIRECTION('',(0.,-1.,0.));
#6751=DIRECTION('',(0.,0.,-1.));
#6752=DIRECTION('',(0.,-1.,0.));
#6753=DIRECTION('',(0.,0.,-1.));
#6754=DIRECTION('',(0.,-1.,0.));
#6755=DIRECTION('',(0.,0.,1.));
#6756=DIRECTION('',(0.,-1.,0.));
#6757=DIRECTION('',(0.,0.,1.));
#6758=DIRECTION('',(0.,-1.,0.));
#6759=DIRECTION('',(0.,0.,-1.));
#6760=DIRECTION('center_axis',(1.,0.,0.));
#6761=DIRECTION('ref_axis',(0.,-0.707106781186545,0.70710678118655));
#6762=DIRECTION('',(0.,-1.,0.));
#6763=DIRECTION('',(0.,0.,-1.));
#6764=DIRECTION('center_axis',(1.,0.,0.));
#6765=DIRECTION('ref_axis',(0.,-0.70710678118655,0.707106781186545));
#6766=DIRECTION('',(0.,-1.,0.));
#6767=DIRECTION('',(0.,0.,-1.));
#6768=DIRECTION('',(0.,1.,0.));
#6769=DIRECTION('center_axis',(1.,0.,0.));
#6770=DIRECTION('ref_axis',(0.,-1.,0.));
#6771=DIRECTION('center_axis',(1.,0.,0.));
#6772=DIRECTION('ref_axis',(0.,1.,0.));
#6773=DIRECTION('',(-1.,0.,0.));
#6774=DIRECTION('center_axis',(1.,0.,0.));
#6775=DIRECTION('ref_axis',(0.,1.,0.));
#6776=DIRECTION('center_axis',(1.,0.,0.));
#6777=DIRECTION('ref_axis',(0.,1.,0.));
#6778=DIRECTION('center_axis',(1.,0.,0.));
#6779=DIRECTION('ref_axis',(0.,0.,-1.));
#6780=DIRECTION('center_axis',(-1.,0.,0.));
#6781=DIRECTION('ref_axis',(0.,-1.,0.));
#6782=DIRECTION('center_axis',(0.,-1.,0.));
#6783=DIRECTION('ref_axis',(0.,0.,1.));
#6784=DIRECTION('center_axis',(-1.,0.,0.));
#6785=DIRECTION('ref_axis',(0.,-1.,0.));
#6786=DIRECTION('center_axis',(-1.,0.,0.));
#6787=DIRECTION('ref_axis',(0.,-1.,0.));
#6788=DIRECTION('',(-1.,0.,0.));
#6789=DIRECTION('center_axis',(1.,0.,0.));
#6790=DIRECTION('ref_axis',(0.,-1.,0.));
#6791=DIRECTION('center_axis',(1.,0.,0.));
#6792=DIRECTION('ref_axis',(0.,-1.,0.));
#6793=DIRECTION('center_axis',(1.,0.,0.));
#6794=DIRECTION('ref_axis',(0.,0.,-1.));
#6795=DIRECTION('center_axis',(-1.,0.,0.));
#6796=DIRECTION('ref_axis',(0.,1.,0.));
#6797=DIRECTION('center_axis',(0.,-1.,0.));
#6798=DIRECTION('ref_axis',(0.,0.,1.));
#6799=DIRECTION('center_axis',(-1.,0.,0.));
#6800=DIRECTION('ref_axis',(0.,0.,1.));
#6801=DIRECTION('center_axis',(-1.,0.,0.));
#6802=DIRECTION('ref_axis',(0.,0.707106781186545,0.70710678118655));
#6803=DIRECTION('',(0.,1.,0.));
#6804=DIRECTION('',(0.,0.,-1.));
#6805=DIRECTION('',(0.,-1.,0.));
#6806=DIRECTION('',(0.,0.,1.));
#6807=DIRECTION('',(0.,1.,0.));
#6808=DIRECTION('center_axis',(-1.,0.,0.));
#6809=DIRECTION('ref_axis',(0.,-0.70710678118655,0.707106781186545));
#6810=DIRECTION('',(0.,0.,1.));
#6811=DIRECTION('',(0.,1.,0.));
#6812=DIRECTION('center_axis',(-1.,0.,0.));
#6813=DIRECTION('ref_axis',(0.,-0.707106781186545,0.70710678118655));
#6814=DIRECTION('',(0.,0.,1.));
#6815=DIRECTION('',(0.,1.,0.));
#6816=DIRECTION('',(0.,0.,-1.));
#6817=DIRECTION('',(0.,1.,0.));
#6818=DIRECTION('',(0.,0.,-1.));
#6819=DIRECTION('',(0.,1.,0.));
#6820=DIRECTION('',(0.,0.,1.));
#6821=DIRECTION('',(0.,1.,0.));
#6822=DIRECTION('',(0.,0.,1.));
#6823=DIRECTION('',(0.,1.,0.));
#6824=DIRECTION('',(0.,0.,-1.));
#6825=DIRECTION('center_axis',(-1.,0.,0.));
#6826=DIRECTION('ref_axis',(0.,0.707106781186545,0.70710678118655));
#6827=DIRECTION('',(0.,1.,0.));
#6828=DIRECTION('',(0.,0.,-1.));
#6829=DIRECTION('center_axis',(-1.,0.,0.));
#6830=DIRECTION('ref_axis',(0.,-1.,0.));
#6831=DIRECTION('center_axis',(-1.,0.,0.));
#6832=DIRECTION('ref_axis',(0.,0.,1.));
#6833=DIRECTION('center_axis',(0.,-1.,0.));
#6834=DIRECTION('ref_axis',(0.,0.,-1.));
#6835=DIRECTION('center_axis',(0.,0.,-1.));
#6836=DIRECTION('ref_axis',(-1.,0.,0.));
#6837=DIRECTION('center_axis',(0.,0.,1.));
#6838=DIRECTION('ref_axis',(-1.,0.,0.));
#6839=DIRECTION('center_axis',(0.,-1.,0.));
#6840=DIRECTION('ref_axis',(1.,0.,0.));
#6841=DIRECTION('center_axis',(0.,0.,-1.));
#6842=DIRECTION('ref_axis',(-1.,0.,0.));
#6843=DIRECTION('center_axis',(0.,0.,1.));
#6844=DIRECTION('ref_axis',(0.,-1.,0.));
#6845=DIRECTION('',(-1.,0.,0.));
#6846=DIRECTION('',(0.,-1.,0.));
#6847=DIRECTION('',(1.,0.,0.));
#6848=DIRECTION('',(0.,1.,0.));
#6849=DIRECTION('center_axis',(0.,0.,1.));
#6850=DIRECTION('ref_axis',(-1.,0.,0.));
#6851=DIRECTION('center_axis',(0.,0.,1.));
#6852=DIRECTION('ref_axis',(-1.,0.,0.));
#6853=DIRECTION('center_axis',(0.,0.,1.));
#6854=DIRECTION('ref_axis',(-1.,0.,0.));
#6855=DIRECTION('center_axis',(0.,0.,1.));
#6856=DIRECTION('ref_axis',(0.,1.,0.));
#6857=DIRECTION('center_axis',(0.,0.,1.));
#6858=DIRECTION('ref_axis',(0.,1.,0.));
#6859=DIRECTION('center_axis',(0.,0.,1.));
#6860=DIRECTION('ref_axis',(-1.,0.,0.));
#6861=DIRECTION('center_axis',(0.,0.,1.));
#6862=DIRECTION('ref_axis',(-1.,0.,0.));
#6863=DIRECTION('center_axis',(0.,0.,1.));
#6864=DIRECTION('ref_axis',(-1.,0.,0.));
#6865=DIRECTION('center_axis',(0.,0.,1.));
#6866=DIRECTION('ref_axis',(-1.,0.,0.));
#6867=DIRECTION('center_axis',(0.,0.,1.));
#6868=DIRECTION('ref_axis',(-1.,0.,0.));
#6869=DIRECTION('center_axis',(0.,0.,1.));
#6870=DIRECTION('ref_axis',(-1.,0.,0.));
#6871=DIRECTION('center_axis',(0.,0.,1.));
#6872=DIRECTION('ref_axis',(-1.,0.,0.));
#6873=DIRECTION('center_axis',(0.,0.,1.));
#6874=DIRECTION('ref_axis',(-1.,0.,0.));
#6875=DIRECTION('center_axis',(0.,0.,1.));
#6876=DIRECTION('ref_axis',(-1.,0.,0.));
#6877=DIRECTION('center_axis',(0.,0.,1.));
#6878=DIRECTION('ref_axis',(-1.,0.,0.));
#6879=DIRECTION('center_axis',(0.,0.,-1.));
#6880=DIRECTION('ref_axis',(-1.,0.,0.));
#6881=DIRECTION('',(0.,0.,-1.));
#6882=DIRECTION('center_axis',(0.,0.,-1.));
#6883=DIRECTION('ref_axis',(-1.,0.,0.));
#6884=DIRECTION('center_axis',(0.,0.,-1.));
#6885=DIRECTION('ref_axis',(-1.,0.,0.));
#6886=DIRECTION('center_axis',(0.,-1.,0.));
#6887=DIRECTION('ref_axis',(1.,0.,0.));
#6888=DIRECTION('center_axis',(0.,0.,-1.));
#6889=DIRECTION('ref_axis',(-1.,0.,0.));
#6890=DIRECTION('center_axis',(0.,0.,-1.));
#6891=DIRECTION('ref_axis',(-1.,0.,0.));
#6892=DIRECTION('',(0.,0.,-1.));
#6893=DIRECTION('center_axis',(0.,0.,-1.));
#6894=DIRECTION('ref_axis',(-1.,0.,0.));
#6895=DIRECTION('center_axis',(0.,0.,-1.));
#6896=DIRECTION('ref_axis',(-1.,0.,0.));
#6897=DIRECTION('center_axis',(0.,-1.,0.));
#6898=DIRECTION('ref_axis',(1.,0.,0.));
#6899=DIRECTION('center_axis',(0.,0.,-1.));
#6900=DIRECTION('ref_axis',(-1.,0.,0.));
#6901=DIRECTION('center_axis',(0.,0.,-1.));
#6902=DIRECTION('ref_axis',(-1.,0.,0.));
#6903=DIRECTION('',(0.,0.,-1.));
#6904=DIRECTION('center_axis',(0.,0.,-1.));
#6905=DIRECTION('ref_axis',(-1.,0.,0.));
#6906=DIRECTION('center_axis',(0.,0.,-1.));
#6907=DIRECTION('ref_axis',(-1.,0.,0.));
#6908=DIRECTION('center_axis',(0.,-1.,0.));
#6909=DIRECTION('ref_axis',(1.,0.,0.));
#6910=DIRECTION('center_axis',(0.,0.,-1.));
#6911=DIRECTION('ref_axis',(-1.,0.,0.));
#6912=DIRECTION('center_axis',(0.,0.,-1.));
#6913=DIRECTION('ref_axis',(-1.,0.,0.));
#6914=DIRECTION('',(0.,0.,-1.));
#6915=DIRECTION('center_axis',(0.,0.,-1.));
#6916=DIRECTION('ref_axis',(-1.,0.,0.));
#6917=DIRECTION('center_axis',(0.,0.,-1.));
#6918=DIRECTION('ref_axis',(-1.,0.,0.));
#6919=DIRECTION('center_axis',(0.,-1.,0.));
#6920=DIRECTION('ref_axis',(1.,0.,0.));
#6921=DIRECTION('center_axis',(0.,0.,-1.));
#6922=DIRECTION('ref_axis',(-1.,0.,0.));
#6923=DIRECTION('center_axis',(0.,0.,-1.));
#6924=DIRECTION('ref_axis',(-1.,0.,0.));
#6925=DIRECTION('',(0.,0.,-1.));
#6926=DIRECTION('center_axis',(0.,0.,-1.));
#6927=DIRECTION('ref_axis',(-1.,0.,0.));
#6928=DIRECTION('center_axis',(0.,0.,-1.));
#6929=DIRECTION('ref_axis',(-1.,0.,0.));
#6930=DIRECTION('center_axis',(0.,-1.,0.));
#6931=DIRECTION('ref_axis',(1.,0.,0.));
#6932=DIRECTION('center_axis',(0.,0.,-1.));
#6933=DIRECTION('ref_axis',(-1.,0.,0.));
#6934=DIRECTION('center_axis',(0.,0.,-1.));
#6935=DIRECTION('ref_axis',(-1.,0.,0.));
#6936=DIRECTION('',(0.,0.,-1.));
#6937=DIRECTION('center_axis',(0.,0.,-1.));
#6938=DIRECTION('ref_axis',(-1.,0.,0.));
#6939=DIRECTION('center_axis',(0.,0.,-1.));
#6940=DIRECTION('ref_axis',(-1.,0.,0.));
#6941=DIRECTION('center_axis',(0.,-1.,0.));
#6942=DIRECTION('ref_axis',(1.,0.,0.));
#6943=DIRECTION('center_axis',(0.,0.,-1.));
#6944=DIRECTION('ref_axis',(-1.,0.,0.));
#6945=DIRECTION('center_axis',(0.,0.,-1.));
#6946=DIRECTION('ref_axis',(-1.,0.,0.));
#6947=DIRECTION('',(0.,0.,-1.));
#6948=DIRECTION('center_axis',(0.,0.,-1.));
#6949=DIRECTION('ref_axis',(-1.,0.,0.));
#6950=DIRECTION('center_axis',(0.,0.,-1.));
#6951=DIRECTION('ref_axis',(-1.,0.,0.));
#6952=DIRECTION('center_axis',(0.,-1.,0.));
#6953=DIRECTION('ref_axis',(1.,0.,0.));
#6954=DIRECTION('center_axis',(0.,0.,-1.));
#6955=DIRECTION('ref_axis',(0.,1.,0.));
#6956=DIRECTION('center_axis',(0.,0.,-1.));
#6957=DIRECTION('ref_axis',(0.,1.,0.));
#6958=DIRECTION('center_axis',(0.,0.,-1.));
#6959=DIRECTION('ref_axis',(0.,1.,0.));
#6960=DIRECTION('',(0.,0.,-1.));
#6961=DIRECTION('center_axis',(0.,0.,-1.));
#6962=DIRECTION('ref_axis',(0.,1.,0.));
#6963=DIRECTION('center_axis',(0.,0.,-1.));
#6964=DIRECTION('ref_axis',(-1.,0.,0.));
#6965=DIRECTION('center_axis',(0.,-1.,0.));
#6966=DIRECTION('ref_axis',(1.,0.,0.));
#6967=DIRECTION('center_axis',(0.,0.,-1.));
#6968=DIRECTION('ref_axis',(-1.,0.,0.));
#6969=DIRECTION('center_axis',(0.,0.,-1.));
#6970=DIRECTION('ref_axis',(-1.,0.,0.));
#6971=DIRECTION('',(0.,0.,-1.));
#6972=DIRECTION('center_axis',(0.,0.,-1.));
#6973=DIRECTION('ref_axis',(-1.,0.,0.));
#6974=DIRECTION('center_axis',(0.,0.,-1.));
#6975=DIRECTION('ref_axis',(-1.,0.,0.));
#6976=DIRECTION('center_axis',(0.,-1.,0.));
#6977=DIRECTION('ref_axis',(1.,0.,0.));
#6978=DIRECTION('center_axis',(0.,0.,-1.));
#6979=DIRECTION('ref_axis',(0.,1.,0.));
#6980=DIRECTION('center_axis',(0.,0.,-1.));
#6981=DIRECTION('ref_axis',(0.,1.,0.));
#6982=DIRECTION('center_axis',(0.,0.,-1.));
#6983=DIRECTION('ref_axis',(0.,1.,0.));
#6984=DIRECTION('',(0.,0.,-1.));
#6985=DIRECTION('center_axis',(0.,0.,-1.));
#6986=DIRECTION('ref_axis',(0.,1.,0.));
#6987=DIRECTION('center_axis',(0.,0.,-1.));
#6988=DIRECTION('ref_axis',(-1.,0.,0.));
#6989=DIRECTION('center_axis',(0.,-1.,0.));
#6990=DIRECTION('ref_axis',(1.,0.,0.));
#6991=DIRECTION('center_axis',(0.,0.,-1.));
#6992=DIRECTION('ref_axis',(-1.,0.,0.));
#6993=DIRECTION('center_axis',(0.,0.,-1.));
#6994=DIRECTION('ref_axis',(-1.,0.,0.));
#6995=DIRECTION('',(0.,0.,-1.));
#6996=DIRECTION('center_axis',(0.,0.,-1.));
#6997=DIRECTION('ref_axis',(-1.,0.,0.));
#6998=DIRECTION('center_axis',(0.,0.,-1.));
#6999=DIRECTION('ref_axis',(-1.,0.,0.));
#7000=DIRECTION('center_axis',(0.,-1.,0.));
#7001=DIRECTION('ref_axis',(1.,0.,0.));
#7002=DIRECTION('center_axis',(0.,0.,-1.));
#7003=DIRECTION('ref_axis',(-1.,0.,0.));
#7004=DIRECTION('center_axis',(0.,0.,-1.));
#7005=DIRECTION('ref_axis',(-1.,0.,0.));
#7006=DIRECTION('',(0.,0.,-1.));
#7007=DIRECTION('center_axis',(0.,0.,-1.));
#7008=DIRECTION('ref_axis',(-1.,0.,0.));
#7009=DIRECTION('center_axis',(0.,0.,-1.));
#7010=DIRECTION('ref_axis',(-1.,0.,0.));
#7011=DIRECTION('center_axis',(0.,-1.,0.));
#7012=DIRECTION('ref_axis',(1.,0.,0.));
#7013=DIRECTION('center_axis',(0.,0.,-1.));
#7014=DIRECTION('ref_axis',(-1.,0.,0.));
#7015=DIRECTION('center_axis',(0.,0.,-1.));
#7016=DIRECTION('ref_axis',(-1.,0.,0.));
#7017=DIRECTION('',(0.,0.,-1.));
#7018=DIRECTION('center_axis',(0.,0.,-1.));
#7019=DIRECTION('ref_axis',(-1.,0.,0.));
#7020=DIRECTION('center_axis',(0.,0.,-1.));
#7021=DIRECTION('ref_axis',(-1.,0.,0.));
#7022=DIRECTION('center_axis',(0.,-1.,0.));
#7023=DIRECTION('ref_axis',(1.,0.,0.));
#7024=DIRECTION('center_axis',(0.,0.,-1.));
#7025=DIRECTION('ref_axis',(-1.,0.,0.));
#7026=DIRECTION('center_axis',(0.,0.,-1.));
#7027=DIRECTION('ref_axis',(-1.,0.,0.));
#7028=DIRECTION('',(0.,0.,-1.));
#7029=DIRECTION('center_axis',(0.,0.,-1.));
#7030=DIRECTION('ref_axis',(-1.,0.,0.));
#7031=DIRECTION('center_axis',(0.,0.,-1.));
#7032=DIRECTION('ref_axis',(-1.,0.,0.));
#7033=DIRECTION('center_axis',(0.,-1.,0.));
#7034=DIRECTION('ref_axis',(1.,0.,0.));
#7035=DIRECTION('center_axis',(0.,0.,-1.));
#7036=DIRECTION('ref_axis',(-1.,0.,0.));
#7037=DIRECTION('center_axis',(0.,0.,-1.));
#7038=DIRECTION('ref_axis',(-1.,0.,0.));
#7039=DIRECTION('',(0.,0.,-1.));
#7040=DIRECTION('center_axis',(0.,0.,-1.));
#7041=DIRECTION('ref_axis',(-1.,0.,0.));
#7042=DIRECTION('center_axis',(0.,0.,-1.));
#7043=DIRECTION('ref_axis',(-1.,0.,0.));
#7044=DIRECTION('center_axis',(0.,-1.,0.));
#7045=DIRECTION('ref_axis',(1.,0.,0.));
#7046=DIRECTION('center_axis',(0.,0.,-1.));
#7047=DIRECTION('ref_axis',(-1.,0.,0.));
#7048=DIRECTION('center_axis',(0.,0.,-1.));
#7049=DIRECTION('ref_axis',(-1.,0.,0.));
#7050=DIRECTION('',(0.,0.,-1.));
#7051=DIRECTION('center_axis',(0.,0.,-1.));
#7052=DIRECTION('ref_axis',(-1.,0.,0.));
#7053=DIRECTION('center_axis',(0.,1.,0.));
#7054=DIRECTION('ref_axis',(0.70710678118655,0.,-0.707106781186545));
#7055=DIRECTION('center_axis',(0.,0.707106781186545,0.70710678118655));
#7056=DIRECTION('ref_axis',(0.,-0.70710678118655,0.707106781186545));
#7057=DIRECTION('',(0.,1.,0.));
#7058=DIRECTION('center_axis',(0.,0.707106781186545,-0.70710678118655));
#7059=DIRECTION('ref_axis',(0.,0.70710678118655,0.707106781186545));
#7060=DIRECTION('center_axis',(0.,-1.,0.));
#7061=DIRECTION('ref_axis',(-0.70710678118655,0.,-0.707106781186545));
#7062=DIRECTION('center_axis',(0.,-0.707106781186545,0.70710678118655));
#7063=DIRECTION('ref_axis',(0.,0.70710678118655,0.707106781186545));
#7064=DIRECTION('',(0.,-1.,0.));
#7065=DIRECTION('center_axis',(0.,-0.707106781186545,-0.70710678118655));
#7066=DIRECTION('ref_axis',(0.,0.70710678118655,-0.707106781186545));
#7067=DIRECTION('center_axis',(0.,0.,1.));
#7068=DIRECTION('ref_axis',(-0.707106781186553,-0.707106781186542,0.));
#7069=DIRECTION('center_axis',(0.,-0.707106781186548,0.707106781186548));
#7070=DIRECTION('ref_axis',(0.,-0.707106781186547,-0.707106781186547));
#7071=DIRECTION('',(0.,0.,1.));
#7072=DIRECTION('center_axis',(0.,0.,-1.));
#7073=DIRECTION('ref_axis',(0.707106781186553,0.707106781186542,0.));
#7074=DIRECTION('center_axis',(0.,0.707106781186548,0.707106781186548));
#7075=DIRECTION('ref_axis',(0.,-0.707106781186547,0.707106781186547));
#7076=DIRECTION('',(0.,0.,1.));
#7077=DIRECTION('center_axis',(0.,-1.,0.));
#7078=DIRECTION('ref_axis',(-0.70710678118655,0.,-0.707106781186545));
#7079=DIRECTION('center_axis',(0.,-0.707106781186548,0.707106781186548));
#7080=DIRECTION('ref_axis',(0.,0.707106781186548,0.707106781186548));
#7081=DIRECTION('',(0.,-1.,0.));
#7082=DIRECTION('center_axis',(0.,-1.,0.));
#7083=DIRECTION('ref_axis',(0.70710678118655,0.,-0.707106781186545));
#7084=DIRECTION('center_axis',(0.,0.707106781186548,0.707106781186548));
#7085=DIRECTION('ref_axis',(0.,0.707106781186548,-0.707106781186548));
#7086=DIRECTION('',(0.,1.,0.));
#7087=DIRECTION('center_axis',(0.,1.,0.));
#7088=DIRECTION('ref_axis',(-0.70710678118655,0.,-0.707106781186545));
#7089=DIRECTION('',(0.,-1.,0.));
#7090=DIRECTION('center_axis',(0.,0.707106781186548,0.707106781186548));
#7091=DIRECTION('ref_axis',(0.,-0.707106781186548,0.707106781186548));
#7092=DIRECTION('center_axis',(0.,-0.707106781186548,-0.707106781186548));
#7093=DIRECTION('ref_axis',(0.,-0.707106781186548,0.707106781186548));
#7094=DIRECTION('center_axis',(0.,0.,1.));
#7095=DIRECTION('ref_axis',(-0.707106781186553,-0.707106781186542,0.));
#7096=DIRECTION('center_axis',(0.,-0.707106781186548,0.707106781186548));
#7097=DIRECTION('ref_axis',(0.,-0.707106781186547,-0.707106781186547));
#7098=DIRECTION('',(0.,0.,1.));
#7099=DIRECTION('center_axis',(0.408248290463863,-0.816496580927726,-0.408248290463863));
#7100=DIRECTION('ref_axis',(0.577350269189625,0.577350269189625,-0.577350269189628));
#7101=DIRECTION('center_axis',(0.,1.,0.));
#7102=DIRECTION('ref_axis',(0.,0.,-1.));
#7103=DIRECTION('center_axis',(1.,0.,0.));
#7104=DIRECTION('ref_axis',(0.,1.,0.));
#7105=DIRECTION('center_axis',(0.,0.,-1.));
#7106=DIRECTION('ref_axis',(1.,0.,0.));
#7107=DIRECTION('center_axis',(-0.408248290463859,-0.816496580927729,-0.408248290463862));
#7108=DIRECTION('ref_axis',(-0.577350269189624,0.577350269189624,-0.57735026918963));
#7109=DIRECTION('center_axis',(0.,0.,-1.));
#7110=DIRECTION('ref_axis',(0.,1.,0.));
#7111=DIRECTION('center_axis',(-1.,0.,0.));
#7112=DIRECTION('ref_axis',(0.,0.,-1.));
#7113=DIRECTION('center_axis',(0.,1.,0.));
#7114=DIRECTION('ref_axis',(-1.,0.,0.));
#7115=DIRECTION('center_axis',(1.,0.,0.));
#7116=DIRECTION('ref_axis',(0.,0.70710678118654,-0.707106781186555));
#7117=DIRECTION('',(-1.,0.,0.));
#7118=DIRECTION('',(1.,0.,0.));
#7119=DIRECTION('center_axis',(0.,-1.,0.));
#7120=DIRECTION('ref_axis',(-0.70710678118655,0.,-0.707106781186545));
#7121=DIRECTION('',(0.,-1.,0.));
#7122=DIRECTION('center_axis',(-0.408248290463863,-0.816496580927726,0.408248290463863));
#7123=DIRECTION('ref_axis',(0.577350269189625,-0.577350269189625,-0.577350269189628));
#7124=DIRECTION('center_axis',(1.,0.,0.));
#7125=DIRECTION('ref_axis',(0.,0.,-1.));
#7126=DIRECTION('center_axis',(0.,-1.,0.));
#7127=DIRECTION('ref_axis',(1.,0.,0.));
#7128=DIRECTION('center_axis',(0.,0.,-1.));
#7129=DIRECTION('ref_axis',(0.,-1.,0.));
#7130=DIRECTION('center_axis',(0.,-1.,0.));
#7131=DIRECTION('ref_axis',(0.70710678118655,0.,-0.707106781186545));
#7132=DIRECTION('',(0.,1.,0.));
#7133=DIRECTION('center_axis',(0.,-0.707106781186548,-0.707106781186548));
#7134=DIRECTION('ref_axis',(0.,0.707106781186548,-0.707106781186548));
#7135=DIRECTION('center_axis',(-1.,0.,0.));
#7136=DIRECTION('ref_axis',(0.,0.,1.));
#7137=DIRECTION('center_axis',(-1.,0.,0.));
#7138=DIRECTION('ref_axis',(0.,0.,1.));
#7139=DIRECTION('center_axis',(0.,1.,0.));
#7140=DIRECTION('ref_axis',(1.,0.,0.));
#7141=DIRECTION('center_axis',(0.,0.,-1.));
#7142=DIRECTION('ref_axis',(0.,1.,0.));
#7143=DIRECTION('center_axis',(0.408248290463859,-0.816496580927729,0.408248290463862));
#7144=DIRECTION('ref_axis',(-0.577350269189624,-0.577350269189624,-0.57735026918963));
#7145=DIRECTION('center_axis',(0.,0.,-1.));
#7146=DIRECTION('ref_axis',(-1.,0.,0.));
#7147=DIRECTION('center_axis',(0.,-1.,0.));
#7148=DIRECTION('ref_axis',(0.,0.,-1.));
#7149=DIRECTION('center_axis',(-1.,0.,0.));
#7150=DIRECTION('ref_axis',(0.,-1.,0.));
#7151=DIRECTION('center_axis',(0.,1.,0.));
#7152=DIRECTION('ref_axis',(-0.70710678118655,0.,-0.707106781186545));
#7153=DIRECTION('',(0.,-1.,0.));
#7154=DIRECTION('center_axis',(0.,-0.707106781186548,-0.707106781186548));
#7155=DIRECTION('ref_axis',(0.,-0.707106781186548,0.707106781186548));
#7156=DIRECTION('center_axis',(1.,0.,0.));
#7157=DIRECTION('ref_axis',(0.,-0.70710678118654,-0.707106781186555));
#7158=DIRECTION('',(-1.,0.,0.));
#7159=DIRECTION('',(1.,0.,0.));
#7160=DIRECTION('center_axis',(1.,0.,0.));
#7161=DIRECTION('ref_axis',(0.,0.,-1.));
#7162=DIRECTION('center_axis',(1.,0.,0.));
#7163=DIRECTION('ref_axis',(0.,-1.,0.));
#7164=DIRECTION('center_axis',(0.,0.,-1.));
#7165=DIRECTION('ref_axis',(-1.,0.,0.));
#7166=DIRECTION('center_axis',(0.,1.,0.));
#7167=DIRECTION('ref_axis',(0.,0.,-1.));
#7168=DIRECTION('center_axis',(0.,0.,-1.));
#7169=DIRECTION('ref_axis',(-0.707106781186558,0.707106781186537,0.));
#7170=DIRECTION('',(0.,0.,-1.));
#7171=DIRECTION('center_axis',(1.,0.,0.));
#7172=DIRECTION('ref_axis',(0.,0.,-1.));
#7173=DIRECTION('center_axis',(0.,-1.,0.));
#7174=DIRECTION('ref_axis',(0.,0.,-1.));
#7175=DIRECTION('center_axis',(-1.,0.,0.));
#7176=DIRECTION('ref_axis',(0.,1.,0.));
#7177=DIRECTION('center_axis',(0.,0.,-1.));
#7178=DIRECTION('ref_axis',(1.,0.,0.));
#7179=DIRECTION('center_axis',(0.408248290463863,-0.816496580927726,-0.408248290463863));
#7180=DIRECTION('ref_axis',(0.577350269189625,0.577350269189625,-0.577350269189628));
#7181=DIRECTION('center_axis',(0.,1.,0.));
#7182=DIRECTION('ref_axis',(0.,0.,-1.));
#7183=DIRECTION('center_axis',(1.,0.,0.));
#7184=DIRECTION('ref_axis',(0.,1.,0.));
#7185=DIRECTION('center_axis',(0.,0.,-1.));
#7186=DIRECTION('ref_axis',(1.,0.,0.));
#7187=DIRECTION('center_axis',(1.,0.,0.));
#7188=DIRECTION('ref_axis',(0.,0.,-1.));
#7189=DIRECTION('center_axis',(1.,0.,0.));
#7190=DIRECTION('ref_axis',(0.,0.,1.));
#7191=DIRECTION('center_axis',(0.,-1.,0.));
#7192=DIRECTION('ref_axis',(-1.,0.,0.));
#7193=DIRECTION('center_axis',(0.,0.,-1.));
#7194=DIRECTION('ref_axis',(0.,-1.,0.));
#7195=DIRECTION('center_axis',(-0.408248290463859,-0.816496580927729,-0.408248290463862));
#7196=DIRECTION('ref_axis',(-0.577350269189624,0.577350269189624,-0.57735026918963));
#7197=DIRECTION('center_axis',(0.,0.,-1.));
#7198=DIRECTION('ref_axis',(0.,1.,0.));
#7199=DIRECTION('center_axis',(-1.,0.,0.));
#7200=DIRECTION('ref_axis',(0.,0.,-1.));
#7201=DIRECTION('center_axis',(0.,1.,0.));
#7202=DIRECTION('ref_axis',(-1.,0.,0.));
#7203=DIRECTION('center_axis',(1.,0.,0.));
#7204=DIRECTION('ref_axis',(0.,0.70710678118655,-0.707106781186545));
#7205=DIRECTION('',(-1.,0.,0.));
#7206=DIRECTION('',(1.,0.,0.));
#7207=DIRECTION('center_axis',(0.,-1.,0.));
#7208=DIRECTION('ref_axis',(-0.70710678118655,0.,-0.707106781186545));
#7209=DIRECTION('',(0.,-1.,0.));
#7210=DIRECTION('center_axis',(-0.40824829046385,-0.816496580927735,0.408248290463859));
#7211=DIRECTION('ref_axis',(0.577350269189634,-0.57735026918961,-0.577350269189634));
#7212=DIRECTION('center_axis',(0.,0.,-1.));
#7213=DIRECTION('ref_axis',(0.,-1.,0.));
#7214=DIRECTION('center_axis',(1.,0.,0.));
#7215=DIRECTION('ref_axis',(0.,0.,-1.));
#7216=DIRECTION('center_axis',(0.,-1.,1.48029736616687E-14));
#7217=DIRECTION('ref_axis',(1.,0.,0.));
#7218=DIRECTION('center_axis',(-1.,0.,0.));
#7219=DIRECTION('ref_axis',(0.,0.,1.));
#7220=DIRECTION('center_axis',(-1.,0.,0.));
#7221=DIRECTION('ref_axis',(0.,0.,1.));
#7222=DIRECTION('center_axis',(0.,1.,0.));
#7223=DIRECTION('ref_axis',(1.,0.,0.));
#7224=DIRECTION('center_axis',(0.,0.,-1.));
#7225=DIRECTION('ref_axis',(0.,1.,0.));
#7226=DIRECTION('center_axis',(0.408248290463855,-0.816496580927734,0.408248290463855));
#7227=DIRECTION('ref_axis',(-0.577350269189634,-0.57735026918961,-0.577350269189634));
#7228=DIRECTION('center_axis',(-1.48029736616688E-14,-1.,0.));
#7229=DIRECTION('ref_axis',(0.,0.,-1.));
#7230=DIRECTION('center_axis',(-1.,0.,0.));
#7231=DIRECTION('ref_axis',(0.,-1.,0.));
#7232=DIRECTION('center_axis',(0.,0.,-1.));
#7233=DIRECTION('ref_axis',(-1.,0.,0.));
#7234=DIRECTION('center_axis',(1.,0.,0.));
#7235=DIRECTION('ref_axis',(0.,-0.70710678118654,-0.707106781186555));
#7236=DIRECTION('',(-1.,0.,0.));
#7237=DIRECTION('',(1.,0.,0.));
#7238=DIRECTION('center_axis',(1.,0.,0.));
#7239=DIRECTION('ref_axis',(0.,0.,-1.));
#7240=DIRECTION('center_axis',(1.,0.,0.));
#7241=DIRECTION('ref_axis',(0.,-1.,0.));
#7242=DIRECTION('center_axis',(0.,0.,-1.));
#7243=DIRECTION('ref_axis',(-1.,0.,0.));
#7244=DIRECTION('center_axis',(0.,1.,0.));
#7245=DIRECTION('ref_axis',(0.,0.,-1.));
#7246=DIRECTION('center_axis',(0.,0.,-1.));
#7247=DIRECTION('ref_axis',(-0.707106781186547,0.707106781186547,0.));
#7248=DIRECTION('',(0.,0.,-1.));
#7249=DIRECTION('center_axis',(-1.,0.,0.));
#7250=DIRECTION('ref_axis',(0.,0.,1.));
#7251=DIRECTION('center_axis',(-1.,0.,0.));
#7252=DIRECTION('ref_axis',(0.,1.,0.));
#7253=DIRECTION('center_axis',(0.,0.,-1.));
#7254=DIRECTION('ref_axis',(1.,0.,0.));
#7255=DIRECTION('center_axis',(0.,-1.,0.));
#7256=DIRECTION('ref_axis',(0.,0.,-1.));
#7257=DIRECTION('center_axis',(0.,0.,1.));
#7258=DIRECTION('ref_axis',(0.707106781186547,-0.707106781186547,0.));
#7259=DIRECTION('',(0.,0.,-1.));
#7260=DIRECTION('center_axis',(0.408248290463863,-0.816496580927726,-0.408248290463863));
#7261=DIRECTION('ref_axis',(0.577350269189626,0.577350269189626,-0.577350269189626));
#7262=DIRECTION('center_axis',(0.,1.,0.));
#7263=DIRECTION('ref_axis',(0.,0.,-1.));
#7264=DIRECTION('center_axis',(1.,0.,0.));
#7265=DIRECTION('ref_axis',(0.,1.,0.));
#7266=DIRECTION('center_axis',(0.,0.,-1.));
#7267=DIRECTION('ref_axis',(1.,0.,0.));
#7268=DIRECTION('center_axis',(1.,0.,0.));
#7269=DIRECTION('ref_axis',(0.,0.,-1.));
#7270=DIRECTION('center_axis',(1.,0.,0.));
#7271=DIRECTION('ref_axis',(0.,0.,1.));
#7272=DIRECTION('center_axis',(0.,-1.,0.));
#7273=DIRECTION('ref_axis',(-1.,0.,0.));
#7274=DIRECTION('center_axis',(0.,0.,-1.));
#7275=DIRECTION('ref_axis',(0.,-1.,0.));
#7276=DIRECTION('center_axis',(-0.408248290463858,-0.816496580927728,-0.408248290463864));
#7277=DIRECTION('ref_axis',(-0.577350269189624,0.577350269189624,-0.57735026918963));
#7278=DIRECTION('center_axis',(0.,0.,-1.));
#7279=DIRECTION('ref_axis',(0.,1.,0.));
#7280=DIRECTION('center_axis',(-1.,0.,0.));
#7281=DIRECTION('ref_axis',(0.,0.,-1.));
#7282=DIRECTION('center_axis',(0.,1.,0.));
#7283=DIRECTION('ref_axis',(-1.,0.,0.));
#7284=DIRECTION('center_axis',(1.,0.,0.));
#7285=DIRECTION('ref_axis',(0.,0.70710678118654,-0.707106781186555));
#7286=DIRECTION('',(-1.,0.,0.));
#7287=DIRECTION('',(1.,0.,0.));
#7288=DIRECTION('center_axis',(0.,-1.,0.));
#7289=DIRECTION('ref_axis',(-0.70710678118655,0.,-0.707106781186545));
#7290=DIRECTION('',(0.,-1.,0.));
#7291=DIRECTION('center_axis',(-0.408248290463858,-0.816496580927728,0.408248290463864));
#7292=DIRECTION('ref_axis',(0.577350269189624,-0.577350269189624,-0.57735026918963));
#7293=DIRECTION('center_axis',(0.,0.,-1.));
#7294=DIRECTION('ref_axis',(0.,-1.,0.));
#7295=DIRECTION('center_axis',(1.,0.,0.));
#7296=DIRECTION('ref_axis',(0.,0.,-1.));
#7297=DIRECTION('center_axis',(0.,-1.,0.));
#7298=DIRECTION('ref_axis',(1.,0.,0.));
#7299=DIRECTION('center_axis',(0.408248290463858,-0.816496580927728,0.408248290463864));
#7300=DIRECTION('ref_axis',(0.577350269189624,0.577350269189624,0.57735026918963));
#7301=DIRECTION('center_axis',(0.,0.,1.));
#7302=DIRECTION('ref_axis',(0.,1.,0.));
#7303=DIRECTION('center_axis',(1.,0.,0.));
#7304=DIRECTION('ref_axis',(0.,0.,1.));
#7305=DIRECTION('center_axis',(0.,1.,0.));
#7306=DIRECTION('ref_axis',(1.,0.,0.));
#7307=DIRECTION('center_axis',(0.408248290463863,-0.816496580927726,0.408248290463863));
#7308=DIRECTION('ref_axis',(-0.577350269189626,-0.577350269189626,-0.577350269189626));
#7309=DIRECTION('center_axis',(0.,-1.,0.));
#7310=DIRECTION('ref_axis',(0.,0.,-1.));
#7311=DIRECTION('center_axis',(-1.,0.,0.));
#7312=DIRECTION('ref_axis',(0.,-1.,0.));
#7313=DIRECTION('center_axis',(0.,0.,-1.));
#7314=DIRECTION('ref_axis',(-1.,0.,0.));
#7315=DIRECTION('center_axis',(1.,0.,0.));
#7316=DIRECTION('ref_axis',(0.,-0.70710678118654,-0.707106781186555));
#7317=DIRECTION('',(-1.,0.,0.));
#7318=DIRECTION('',(1.,0.,0.));
#7319=DIRECTION('center_axis',(-0.408248290463863,-0.816496580927726,0.408248290463863));
#7320=DIRECTION('ref_axis',(-0.577350269189626,0.577350269189626,0.577350269189626));
#7321=DIRECTION('center_axis',(0.,1.,0.));
#7322=DIRECTION('ref_axis',(0.,0.,1.));
#7323=DIRECTION('center_axis',(-1.,0.,0.));
#7324=DIRECTION('ref_axis',(0.,1.,0.));
#7325=DIRECTION('center_axis',(0.,0.,1.));
#7326=DIRECTION('ref_axis',(-1.,0.,0.));
#7327=DIRECTION('center_axis',(1.,0.,0.));
#7328=DIRECTION('ref_axis',(0.,0.707106781186542,0.707106781186553));
#7329=DIRECTION('',(-1.,0.,0.));
#7330=DIRECTION('center_axis',(0.,0.,-1.));
#7331=DIRECTION('ref_axis',(-0.707106781186558,0.707106781186537,0.));
#7332=DIRECTION('',(0.,0.,-1.));
#7333=DIRECTION('center_axis',(-0.408248290463853,-0.81649658092773,-0.408248290463865));
#7334=DIRECTION('ref_axis',(0.577350269189624,-0.577350269189624,0.57735026918963));
#7335=DIRECTION('center_axis',(0.,-1.,0.));
#7336=DIRECTION('ref_axis',(0.,0.,1.));
#7337=DIRECTION('center_axis',(1.,0.,0.));
#7338=DIRECTION('ref_axis',(0.,-1.,0.));
#7339=DIRECTION('center_axis',(0.,-7.40148683083442E-15,1.));
#7340=DIRECTION('ref_axis',(1.,0.,0.));
#7341=DIRECTION('center_axis',(0.408248290463858,-0.816496580927728,-0.408248290463864));
#7342=DIRECTION('ref_axis',(-0.57735026918962,-0.57735026918962,0.577350269189638));
#7343=DIRECTION('center_axis',(7.40148683083442E-15,0.,1.));
#7344=DIRECTION('ref_axis',(0.,-1.,0.));
#7345=DIRECTION('center_axis',(-1.,0.,0.));
#7346=DIRECTION('ref_axis',(0.,0.,1.));
#7347=DIRECTION('center_axis',(0.,-1.,0.));
#7348=DIRECTION('ref_axis',(-1.,0.,0.));
#7349=DIRECTION('center_axis',(1.,0.,0.));
#7350=DIRECTION('ref_axis',(0.,-0.707106781186537,0.707106781186558));
#7351=DIRECTION('',(1.,0.,0.));
#7352=DIRECTION('center_axis',(0.,1.,0.));
#7353=DIRECTION('ref_axis',(-0.707106781186553,0.,0.707106781186542));
#7354=DIRECTION('center_axis',(0.,0.,1.));
#7355=DIRECTION('ref_axis',(-0.707106781186558,-0.707106781186537,0.));
#7356=DIRECTION('',(0.,0.,1.));
#7357=DIRECTION('center_axis',(0.,0.,-1.));
#7358=DIRECTION('ref_axis',(0.707106781186558,-0.707106781186537,0.));
#7359=DIRECTION('',(0.,0.,-1.));
#7360=DIRECTION('center_axis',(0.,-1.,0.));
#7361=DIRECTION('ref_axis',(0.707106781186553,0.,0.707106781186542));
#7362=DIRECTION('center_axis',(0.,-1.,0.));
#7363=DIRECTION('ref_axis',(-0.70710678118655,0.,-0.707106781186545));
#7364=DIRECTION('',(0.,-1.,0.));
#7365=DIRECTION('center_axis',(0.,0.,1.));
#7366=DIRECTION('ref_axis',(0.707106781186558,0.707106781186537,0.));
#7367=DIRECTION('',(0.,0.,1.));
#7368=DIRECTION('center_axis',(0.,1.,0.));
#7369=DIRECTION('ref_axis',(0.70710678118655,0.,-0.707106781186545));
#7370=DIRECTION('',(0.,1.,0.));
#7371=DIRECTION('center_axis',(0.,0.,-1.));
#7372=DIRECTION('ref_axis',(-0.707106781186547,-0.707106781186547,0.));
#7373=DIRECTION('',(0.,0.,1.));
#7374=DIRECTION('center_axis',(1.,0.,0.));
#7375=DIRECTION('ref_axis',(0.,0.70710678118655,0.707106781186545));
#7376=DIRECTION('',(-1.,0.,0.));
#7377=DIRECTION('',(1.,0.,0.));
#7378=DIRECTION('center_axis',(0.,1.,0.));
#7379=DIRECTION('ref_axis',(0.70710678118655,0.,-0.707106781186545));
#7380=DIRECTION('',(0.,1.,0.));
#7381=DIRECTION('center_axis',(-1.,0.,0.));
#7382=DIRECTION('ref_axis',(0.,-0.70710678118655,0.707106781186545));
#7383=DIRECTION('',(1.,0.,0.));
#7384=DIRECTION('',(-1.,0.,0.));
#7385=DIRECTION('center_axis',(0.,1.,0.));
#7386=DIRECTION('ref_axis',(-0.70710678118655,0.,-0.707106781186545));
#7387=DIRECTION('',(0.,-1.,0.));
#7388=DIRECTION('center_axis',(0.,0.,1.));
#7389=DIRECTION('ref_axis',(0.707106781186547,0.707106781186547,0.));
#7390=DIRECTION('',(0.,0.,1.));
#7391=DIRECTION('center_axis',(0.,-1.,0.));
#7392=DIRECTION('ref_axis',(0.70710678118655,0.,-0.707106781186545));
#7393=DIRECTION('',(0.,1.,0.));
#7394=DIRECTION('center_axis',(0.,0.,-1.));
#7395=DIRECTION('ref_axis',(-0.707106781186558,-0.707106781186537,0.));
#7396=DIRECTION('',(0.,0.,1.));
#7397=DIRECTION('center_axis',(1.,0.,0.));
#7398=DIRECTION('ref_axis',(0.,0.70710678118654,0.707106781186555));
#7399=DIRECTION('',(-1.,0.,0.));
#7400=DIRECTION('',(1.,0.,0.));
#7401=DIRECTION('center_axis',(0.,1.,0.));
#7402=DIRECTION('ref_axis',(0.70710678118655,0.,-0.707106781186545));
#7403=DIRECTION('',(0.,1.,0.));
#7404=DIRECTION('center_axis',(0.,0.,1.));
#7405=DIRECTION('ref_axis',(0.707106781186558,-0.707106781186537,0.));
#7406=DIRECTION('',(0.,0.,-1.));
#7407=DIRECTION('center_axis',(-1.,0.,0.));
#7408=DIRECTION('ref_axis',(0.,-0.70710678118654,0.707106781186555));
#7409=DIRECTION('',(1.,0.,0.));
#7410=DIRECTION('',(-1.,0.,0.));
#7411=DIRECTION('center_axis',(0.,0.,1.));
#7412=DIRECTION('ref_axis',(0.707106781186558,0.707106781186537,0.));
#7413=DIRECTION('',(0.,0.,1.));
#7414=DIRECTION('center_axis',(0.,0.,1.));
#7415=DIRECTION('ref_axis',(-0.707106781186553,0.707106781186542,0.));
#7416=DIRECTION('',(0.,0.,-1.));
#7417=DIRECTION('center_axis',(0.,1.,0.));
#7418=DIRECTION('ref_axis',(0.70710678118655,0.,-0.707106781186545));
#7419=DIRECTION('',(0.,1.,0.));
#7420=DIRECTION('center_axis',(0.,0.707106781186548,-0.707106781186548));
#7421=DIRECTION('ref_axis',(0.,-0.707106781186548,-0.707106781186548));
#7422=DIRECTION('center_axis',(0.,0.,-1.));
#7423=DIRECTION('ref_axis',(0.707106781186553,0.707106781186542,0.));
#7424=DIRECTION('',(0.,0.,1.));
#7425=DIRECTION('center_axis',(0.,0.,-1.));
#7426=DIRECTION('ref_axis',(0.707106781186553,-0.707106781186542,0.));
#7427=DIRECTION('',(0.,0.,-1.));
#7428=DIRECTION('center_axis',(0.,0.707106781186548,-0.707106781186548));
#7429=DIRECTION('ref_axis',(0.,0.707106781186547,0.707106781186547));
#7430=DIRECTION('center_axis',(0.,0.,1.));
#7431=DIRECTION('ref_axis',(-0.707106781186553,0.707106781186542,0.));
#7432=DIRECTION('',(0.,0.,-1.));
#7433=DIRECTION('center_axis',(0.,1.,0.));
#7434=DIRECTION('ref_axis',(0.70710678118655,0.,-0.707106781186545));
#7435=DIRECTION('',(0.,1.,0.));
#7436=DIRECTION('center_axis',(0.,0.707106781186548,-0.707106781186548));
#7437=DIRECTION('ref_axis',(0.,-0.707106781186548,-0.707106781186548));
#7438=DIRECTION('center_axis',(0.,0.,-1.));
#7439=DIRECTION('ref_axis',(0.707106781186553,-0.707106781186542,0.));
#7440=DIRECTION('',(0.,0.,-1.));
#7441=DIRECTION('center_axis',(0.,-1.,0.));
#7442=DIRECTION('ref_axis',(0.,0.,-1.));
#7443=DIRECTION('',(1.,0.,0.));
#7444=DIRECTION('',(-1.,0.,0.));
#7445=DIRECTION('center_axis',(0.,0.,-1.));
#7446=DIRECTION('ref_axis',(0.,1.,0.));
#7447=DIRECTION('',(-1.,0.,0.));
#7448=DIRECTION('center_axis',(0.,-1.,0.));
#7449=DIRECTION('ref_axis',(0.,0.,-1.));
#7450=DIRECTION('',(1.,0.,0.));
#7451=DIRECTION('center_axis',(0.,0.,-1.));
#7452=DIRECTION('ref_axis',(0.,1.,0.));
#7453=DIRECTION('',(-1.,0.,0.));
#7454=DIRECTION('center_axis',(0.,-1.,0.));
#7455=DIRECTION('ref_axis',(0.,0.,-1.));
#7456=DIRECTION('',(-1.,0.,0.));
#7457=DIRECTION('center_axis',(0.,0.,1.));
#7458=DIRECTION('ref_axis',(0.,-1.,0.));
#7459=DIRECTION('',(-1.,0.,0.));
#7460=DIRECTION('center_axis',(0.,0.,1.));
#7461=DIRECTION('ref_axis',(0.,-1.,0.));
#7462=DIRECTION('',(-1.,0.,0.));
#7463=DIRECTION('center_axis',(0.,-1.,0.));
#7464=DIRECTION('ref_axis',(0.,0.,-1.));
#7465=DIRECTION('center_axis',(0.,1.,0.));
#7466=DIRECTION('ref_axis',(0.,0.,1.));
#7467=DIRECTION('center_axis',(0.,1.,0.));
#7468=DIRECTION('ref_axis',(0.,0.,1.));
#7469=DIRECTION('center_axis',(0.,0.,-1.));
#7470=DIRECTION('ref_axis',(0.,1.,0.));
#7471=DIRECTION('center_axis',(0.,1.,0.));
#7472=DIRECTION('ref_axis',(0.,0.,1.));
#7473=DIRECTION('center_axis',(0.,0.,1.));
#7474=DIRECTION('ref_axis',(0.,-1.,0.));
#7475=DIRECTION('center_axis',(0.,1.,0.));
#7476=DIRECTION('ref_axis',(0.,0.,1.));
#7477=DIRECTION('center_axis',(0.,0.,-1.));
#7478=DIRECTION('ref_axis',(0.,1.,0.));
#7479=DIRECTION('center_axis',(0.,0.,-1.));
#7480=DIRECTION('ref_axis',(0.,1.,0.));
#7481=DIRECTION('center_axis',(0.,1.,0.));
#7482=DIRECTION('ref_axis',(0.,0.,1.));
#7483=DIRECTION('center_axis',(0.,-1.,0.));
#7484=DIRECTION('ref_axis',(0.,0.,-1.));
#7485=DIRECTION('center_axis',(0.,0.,-1.));
#7486=DIRECTION('ref_axis',(0.,1.,0.));
#7487=DIRECTION('center_axis',(0.,0.,1.));
#7488=DIRECTION('ref_axis',(-1.,0.,0.));
#7489=DIRECTION('center_axis',(0.,0.,1.));
#7490=DIRECTION('ref_axis',(-1.,0.,0.));
#7491=DIRECTION('center_axis',(0.,0.,1.));
#7492=DIRECTION('ref_axis',(-1.,0.,0.));
#7493=DIRECTION('center_axis',(0.,0.,1.));
#7494=DIRECTION('ref_axis',(-1.,0.,0.));
#7495=DIRECTION('center_axis',(0.,0.,1.));
#7496=DIRECTION('ref_axis',(-1.,0.,0.));
#7497=DIRECTION('center_axis',(0.,0.,1.));
#7498=DIRECTION('ref_axis',(-1.,0.,0.));
#7499=DIRECTION('center_axis',(0.,0.,1.));
#7500=DIRECTION('ref_axis',(-1.,0.,0.));
#7501=DIRECTION('center_axis',(0.,0.,1.));
#7502=DIRECTION('ref_axis',(-1.,0.,0.));
#7503=DIRECTION('center_axis',(0.,0.,1.));
#7504=DIRECTION('ref_axis',(-1.,0.,0.));
#7505=DIRECTION('center_axis',(0.,0.,1.));
#7506=DIRECTION('ref_axis',(-1.,0.,0.));
#7507=DIRECTION('center_axis',(0.,0.,1.));
#7508=DIRECTION('ref_axis',(-1.,0.,0.));
#7509=DIRECTION('center_axis',(0.,0.,1.));
#7510=DIRECTION('ref_axis',(-1.,0.,0.));
#7511=DIRECTION('center_axis',(0.,0.,1.));
#7512=DIRECTION('ref_axis',(-1.,0.,0.));
#7513=DIRECTION('center_axis',(0.,0.,1.));
#7514=DIRECTION('ref_axis',(-1.,0.,0.));
#7515=DIRECTION('center_axis',(0.,0.,1.));
#7516=DIRECTION('ref_axis',(-1.,0.,0.));
#7517=DIRECTION('center_axis',(0.,0.,1.));
#7518=DIRECTION('ref_axis',(-1.,0.,0.));
#8751=CARTESIAN_POINT('',(0.,0.,0.));
#8752=CARTESIAN_POINT('Origin',(4.,0.,0.));
#8753=CARTESIAN_POINT('',(4.,-5.13675,6.29070444552017E-16));
#8754=CARTESIAN_POINT('Origin',(4.,0.,0.));
#8755=CARTESIAN_POINT('',(-4.,-5.13675,-6.29070444552017E-16));
#8756=CARTESIAN_POINT('',(4.,-5.13675,6.29070444552017E-16));
#8757=CARTESIAN_POINT('Origin',(-4.,0.,0.));
#8758=CARTESIAN_POINT('Origin',(4.,-10.,8.));
#8759=CARTESIAN_POINT('',(-4.,-10.,8.));
#8760=CARTESIAN_POINT('',(4.,-10.,8.));
#8761=CARTESIAN_POINT('',(2.,-10.,8.));
#8762=CARTESIAN_POINT('',(-4.,-10.,-7.859));
#8763=CARTESIAN_POINT('',(-4.,-10.,8.));
#8764=CARTESIAN_POINT('',(4.,-10.,-7.859));
#8765=CARTESIAN_POINT('',(4.,-10.,-7.859));
#8766=CARTESIAN_POINT('',(4.,-10.,8.));
#8767=CARTESIAN_POINT('Origin',(4.,10.,8.));
#8768=CARTESIAN_POINT('',(4.,10.,8.));
#8769=CARTESIAN_POINT('',(4.,-10.,8.));
#8770=CARTESIAN_POINT('',(4.,10.,-7.859));
#8771=CARTESIAN_POINT('',(4.,10.,-7.859));
#8772=CARTESIAN_POINT('',(4.,10.,8.));
#8773=CARTESIAN_POINT('Origin',(-4.,10.,8.));
#8774=CARTESIAN_POINT('',(-4.,10.,8.));
#8775=CARTESIAN_POINT('',(-2.,10.,8.));
#8776=CARTESIAN_POINT('',(-4.,10.,-7.859));
#8777=CARTESIAN_POINT('',(-4.,10.,-7.859));
#8778=CARTESIAN_POINT('',(-4.,10.,8.));
#8779=CARTESIAN_POINT('Origin',(-4.,-10.,8.));
#8780=CARTESIAN_POINT('',(-4.,-20.,8.));
#8781=CARTESIAN_POINT('',(-4.,-10.,-7.859));
#8782=CARTESIAN_POINT('Origin',(0.,0.,-7.859));
#8783=CARTESIAN_POINT('Origin',(29.7,21.9999999999999,-1.92966607280848));
#8784=CARTESIAN_POINT('',(30.,21.9999999999999,-7.22966607280848));
#8785=CARTESIAN_POINT('Origin',(30.,21.9999999999999,-1.92966607280848));
#8786=CARTESIAN_POINT('',(29.7,21.9999999999999,-6.92966607280848));
#8787=CARTESIAN_POINT('Origin',(29.7,21.9999999999999,-7.22966607280848));
#8788=CARTESIAN_POINT('',(29.7,16.9999999999999,-1.92966607280848));
#8789=CARTESIAN_POINT('Origin',(29.7,21.9999999999999,-1.92966607280848));
#8790=CARTESIAN_POINT('Origin',(29.7,21.9999999999999,-1.92966607280848));
#8791=CARTESIAN_POINT('Origin',(30.,0.,12.));
#8792=CARTESIAN_POINT('',(30.,-29.7,8.3));
#8793=CARTESIAN_POINT('',(30.,-29.7,15.7));
#8794=CARTESIAN_POINT('',(30.,-29.7,14.));
#8795=CARTESIAN_POINT('',(30.,-29.2999999999999,8.3));
#8796=CARTESIAN_POINT('',(30.,-15.,8.3));
#8797=CARTESIAN_POINT('',(30.,-28.6999999999999,7.7));
#8798=CARTESIAN_POINT('Origin',(30.,-29.2999999999999,7.7));
#8799=CARTESIAN_POINT('',(30.,-28.6999999999999,4.3));
#8800=CARTESIAN_POINT('',(30.,-28.6999999999999,8.));
#8801=CARTESIAN_POINT('',(30.,-28.2999999999999,4.3));
#8802=CARTESIAN_POINT('',(30.,-7.49999999999996,4.3));
#8803=CARTESIAN_POINT('',(30.,-27.6999999999999,3.7));
#8804=CARTESIAN_POINT('Origin',(30.,-28.2999999999999,3.7));
#8805=CARTESIAN_POINT('',(30.,-27.6999999999999,-7.55933214561695));
#8806=CARTESIAN_POINT('',(30.,-27.6999999999999,2.07033392719152));
#8807=CARTESIAN_POINT('',(30.,-16.2999999999999,-7.55933214561695));
#8808=CARTESIAN_POINT('',(30.,-7.99999999999996,-7.55933214561695));
#8809=CARTESIAN_POINT('',(30.,-16.2999999999999,4.3));
#8810=CARTESIAN_POINT('',(30.,-16.2999999999999,8.));
#8811=CARTESIAN_POINT('',(30.,-15.2999999999999,4.3));
#8812=CARTESIAN_POINT('',(30.,-7.49999999999996,4.3));
#8813=CARTESIAN_POINT('',(30.,-15.2999999999999,8.3));
#8814=CARTESIAN_POINT('',(30.,-15.2999999999999,10.));
#8815=CARTESIAN_POINT('',(30.,15.2999999999999,8.3));
#8816=CARTESIAN_POINT('',(30.,-15.,8.3));
#8817=CARTESIAN_POINT('',(30.,15.2999999999999,4.3));
#8818=CARTESIAN_POINT('',(30.,15.2999999999999,10.));
#8819=CARTESIAN_POINT('',(30.,16.2999999999999,4.3));
#8820=CARTESIAN_POINT('',(30.,7.49999999999996,4.3));
#8821=CARTESIAN_POINT('',(30.,16.2999999999999,-7.55933214561695));
#8822=CARTESIAN_POINT('',(30.,16.2999999999999,8.));
#8823=CARTESIAN_POINT('',(30.,27.6999999999999,-7.55933214561695));
#8824=CARTESIAN_POINT('',(30.,7.99999999999996,-7.55933214561695));
#8825=CARTESIAN_POINT('',(30.,27.6999999999999,3.7));
#8826=CARTESIAN_POINT('',(30.,27.6999999999999,2.07033392719152));
#8827=CARTESIAN_POINT('',(30.,28.2999999999999,4.3));
#8828=CARTESIAN_POINT('Origin',(30.,28.2999999999999,3.7));
#8829=CARTESIAN_POINT('',(30.,28.6999999999999,4.3));
#8830=CARTESIAN_POINT('',(30.,7.49999999999996,4.3));
#8831=CARTESIAN_POINT('',(30.,28.6999999999999,7.7));
#8832=CARTESIAN_POINT('',(30.,28.6999999999999,8.));
#8833=CARTESIAN_POINT('',(30.,29.2999999999999,8.3));
#8834=CARTESIAN_POINT('Origin',(30.,29.2999999999999,7.7));
#8835=CARTESIAN_POINT('',(30.,29.7,8.3));
#8836=CARTESIAN_POINT('',(30.,-15.,8.3));
#8837=CARTESIAN_POINT('',(30.,29.7,15.7));
#8838=CARTESIAN_POINT('',(30.,29.7,10.));
#8839=CARTESIAN_POINT('',(30.,15.,15.7));
#8840=CARTESIAN_POINT('',(30.,-21.9999999999999,3.37033392719152));
#8841=CARTESIAN_POINT('Origin',(30.,-21.9999999999999,-1.92966607280848));
#8842=CARTESIAN_POINT('Origin',(0.,21.9999999999999,-1.92966607280848));
#8843=CARTESIAN_POINT('',(-29.7,16.9999999999999,-1.92966607280848));
#8844=CARTESIAN_POINT('',(0.,16.9999999999999,-1.92966607280848));
#8845=CARTESIAN_POINT('',(-29.7,21.9999999999999,3.07033392719152));
#8846=CARTESIAN_POINT('Origin',(-29.7,21.9999999999999,-1.92966607280848));
#8847=CARTESIAN_POINT('Origin',(-29.7,21.9999999999999,-1.92966607280848));
#8848=CARTESIAN_POINT('Origin',(29.7,-21.9999999999999,-1.92966607280848));
#8849=CARTESIAN_POINT('',(29.7,-16.9999999999999,-1.92966607280848));
#8850=CARTESIAN_POINT('',(29.7,-21.9999999999999,3.07033392719152));
#8851=CARTESIAN_POINT('Origin',(29.7,-21.9999999999999,-1.92966607280848));
#8852=CARTESIAN_POINT('Origin',(29.7,-21.9999999999999,3.37033392719152));
#8853=CARTESIAN_POINT('Origin',(29.7,-21.9999999999999,-1.92966607280848));
#8854=CARTESIAN_POINT('Origin',(0.,-21.9999999999999,-1.92966607280848));
#8855=CARTESIAN_POINT('',(-29.7,-16.9999999999999,-1.92966607280848));
#8856=CARTESIAN_POINT('',(0.,-16.9999999999999,-1.92966607280848));
#8857=CARTESIAN_POINT('',(-29.7,-21.9999999999999,-6.92966607280848));
#8858=CARTESIAN_POINT('Origin',(-29.7,-21.9999999999999,-1.92966607280848));
#8859=CARTESIAN_POINT('Origin',(-29.7,-21.9999999999999,-1.92966607280848));
#8860=CARTESIAN_POINT('Origin',(-29.7,21.9999999999999,-1.92966607280848));
#8861=CARTESIAN_POINT('',(-30.,21.9999999999999,3.37033392719152));
#8862=CARTESIAN_POINT('Origin',(-30.,21.9999999999999,-1.92966607280848));
#8863=CARTESIAN_POINT('Origin',(-29.7,21.9999999999999,3.37033392719152));
#8864=CARTESIAN_POINT('Origin',(-30.,0.,12.));
#8865=CARTESIAN_POINT('',(-30.,-29.2999999999999,8.3));
#8866=CARTESIAN_POINT('',(-30.,-28.6999999999999,7.7));
#8867=CARTESIAN_POINT('Origin',(-30.,-29.2999999999999,7.7));
#8868=CARTESIAN_POINT('',(-30.,-29.7,8.3));
#8869=CARTESIAN_POINT('',(-30.,-15.,8.3));
#8870=CARTESIAN_POINT('',(-30.,-29.7,15.7));
#8871=CARTESIAN_POINT('',(-30.,-29.7,14.));
#8872=CARTESIAN_POINT('',(-30.,29.7,15.7));
#8873=CARTESIAN_POINT('',(-30.,15.,15.7));
#8874=CARTESIAN_POINT('',(-30.,29.7,8.3));
#8875=CARTESIAN_POINT('',(-30.,29.7,10.));
#8876=CARTESIAN_POINT('',(-30.,29.2999999999999,8.3));
#8877=CARTESIAN_POINT('',(-30.,-15.,8.3));
#8878=CARTESIAN_POINT('',(-30.,28.6999999999999,7.7));
#8879=CARTESIAN_POINT('Origin',(-30.,29.2999999999999,7.7));
#8880=CARTESIAN_POINT('',(-30.,28.6999999999999,4.3));
#8881=CARTESIAN_POINT('',(-30.,28.6999999999999,8.));
#8882=CARTESIAN_POINT('',(-30.,28.2999999999999,4.3));
#8883=CARTESIAN_POINT('',(-30.,7.49999999999996,4.3));
#8884=CARTESIAN_POINT('',(-30.,27.6999999999999,3.7));
#8885=CARTESIAN_POINT('Origin',(-30.,28.2999999999999,3.7));
#8886=CARTESIAN_POINT('',(-30.,27.6999999999999,-7.55933214561695));
#8887=CARTESIAN_POINT('',(-30.,27.6999999999999,2.07033392719152));
#8888=CARTESIAN_POINT('',(-30.,16.2999999999999,-7.55933214561695));
#8889=CARTESIAN_POINT('',(-30.,7.99999999999996,-7.55933214561695));
#8890=CARTESIAN_POINT('',(-30.,16.2999999999999,4.3));
#8891=CARTESIAN_POINT('',(-30.,16.2999999999999,8.));
#8892=CARTESIAN_POINT('',(-30.,15.2999999999999,4.3));
#8893=CARTESIAN_POINT('',(-30.,7.49999999999996,4.3));
#8894=CARTESIAN_POINT('',(-30.,15.2999999999999,8.3));
#8895=CARTESIAN_POINT('',(-30.,15.2999999999999,10.));
#8896=CARTESIAN_POINT('',(-30.,-15.2999999999999,8.3));
#8897=CARTESIAN_POINT('',(-30.,-15.,8.3));
#8898=CARTESIAN_POINT('',(-30.,-15.2999999999999,4.3));
#8899=CARTESIAN_POINT('',(-30.,-15.2999999999999,10.));
#8900=CARTESIAN_POINT('',(-30.,-16.2999999999999,4.3));
#8901=CARTESIAN_POINT('',(-30.,-7.49999999999996,4.3));
#8902=CARTESIAN_POINT('',(-30.,-16.2999999999999,-7.55933214561695));
#8903=CARTESIAN_POINT('',(-30.,-16.2999999999999,8.));
#8904=CARTESIAN_POINT('',(-30.,-27.6999999999999,-7.55933214561695));
#8905=CARTESIAN_POINT('',(-30.,-7.99999999999996,-7.55933214561695));
#8906=CARTESIAN_POINT('',(-30.,-27.6999999999999,3.7));
#8907=CARTESIAN_POINT('',(-30.,-27.6999999999999,2.07033392719152));
#8908=CARTESIAN_POINT('',(-30.,-28.2999999999999,4.3));
#8909=CARTESIAN_POINT('Origin',(-30.,-28.2999999999999,3.7));
#8910=CARTESIAN_POINT('',(-30.,-28.6999999999999,4.3));
#8911=CARTESIAN_POINT('',(-30.,-7.49999999999996,4.3));
#8912=CARTESIAN_POINT('',(-30.,-28.6999999999999,8.));
#8913=CARTESIAN_POINT('',(-30.,-21.9999999999999,-7.22966607280848));
#8914=CARTESIAN_POINT('Origin',(-30.,-21.9999999999999,-1.92966607280848));
#8915=CARTESIAN_POINT('Origin',(-29.7,-21.9999999999999,-1.92966607280848));
#8916=CARTESIAN_POINT('Origin',(-29.7,-21.9999999999999,-7.22966607280848));
#8917=CARTESIAN_POINT('Origin',(-14.1247849194883,-25.3746234146051,15.7));
#8918=CARTESIAN_POINT('',(-12.3247849194883,-25.3746234146051,16.));
#8919=CARTESIAN_POINT('Origin',(-14.1247849194883,-25.3746234146051,16.));
#8920=CARTESIAN_POINT('',(-12.6247849194883,-25.3746234146051,15.7));
#8921=CARTESIAN_POINT('Origin',(-12.3247849194883,-25.3746234146051,15.7));
#8922=CARTESIAN_POINT('Origin',(-14.1247849194883,-25.3746234146051,15.7));
#8923=CARTESIAN_POINT('Origin',(0.,30.,16.));
#8924=CARTESIAN_POINT('',(29.7,-29.7,16.));
#8925=CARTESIAN_POINT('',(-29.7,-29.7,16.));
#8926=CARTESIAN_POINT('',(0.,-29.7,16.));
#8927=CARTESIAN_POINT('',(29.7,29.7,16.));
#8928=CARTESIAN_POINT('',(29.7,15.,16.));
#8929=CARTESIAN_POINT('',(-29.7,29.7,16.));
#8930=CARTESIAN_POINT('',(0.,29.7,16.));
#8931=CARTESIAN_POINT('',(-29.7,15.,16.));
#8932=CARTESIAN_POINT('',(-21.3247849194883,-6.37462341460511,16.));
#8933=CARTESIAN_POINT('Origin',(-23.1247849194883,-6.37462341460511,16.));
#8934=CARTESIAN_POINT('',(15.9247849194883,-25.3746234146051,16.));
#8935=CARTESIAN_POINT('Origin',(14.1247849194883,-25.3746234146051,16.));
#8936=CARTESIAN_POINT('',(24.9247849194883,15.3746234146051,16.));
#8937=CARTESIAN_POINT('Origin',(23.1247849194883,15.3746234146051,16.));
#8938=CARTESIAN_POINT('',(-21.3247849194883,15.3746234146051,16.));
#8939=CARTESIAN_POINT('Origin',(-23.1247849194883,15.3746234146051,16.));
#8940=CARTESIAN_POINT('',(-21.3247849194883,6.37462341460511,16.));
#8941=CARTESIAN_POINT('Origin',(-23.1247849194883,6.37462341460511,16.));
#8942=CARTESIAN_POINT('',(15.9247849194883,25.3746234146051,16.));
#8943=CARTESIAN_POINT('Origin',(14.1247849194883,25.3746234146051,16.));
#8944=CARTESIAN_POINT('',(24.9247849194883,25.3746234146051,16.));
#8945=CARTESIAN_POINT('Origin',(23.1247849194883,25.3746234146051,16.));
#8946=CARTESIAN_POINT('',(-12.3247849194883,25.3746234146051,16.));
#8947=CARTESIAN_POINT('Origin',(-14.1247849194883,25.3746234146051,16.));
#8948=CARTESIAN_POINT('',(-21.3247849194883,25.3746234146051,16.));
#8949=CARTESIAN_POINT('Origin',(-23.1247849194883,25.3746234146051,16.));
#8950=CARTESIAN_POINT('',(24.9247849194883,-25.3746234146051,16.));
#8951=CARTESIAN_POINT('Origin',(23.1247849194883,-25.3746234146051,16.));
#8952=CARTESIAN_POINT('',(24.9247849194883,-15.3746234146051,16.));
#8953=CARTESIAN_POINT('Origin',(23.1247849194883,-15.3746234146051,16.));
#8954=CARTESIAN_POINT('',(-21.3247849194883,-25.3746234146051,16.));
#8955=CARTESIAN_POINT('Origin',(-23.1247849194883,-25.3746234146051,16.));
#8956=CARTESIAN_POINT('',(-21.3247849194883,-15.3746234146051,16.));
#8957=CARTESIAN_POINT('Origin',(-23.1247849194883,-15.3746234146051,16.));
#8958=CARTESIAN_POINT('',(24.9247849194883,6.37462341460511,16.));
#8959=CARTESIAN_POINT('Origin',(23.1247849194883,6.37462341460511,16.));
#8960=CARTESIAN_POINT('',(24.9247849194883,-6.37462341460511,16.));
#8961=CARTESIAN_POINT('Origin',(23.1247849194883,-6.37462341460511,16.));
#8962=CARTESIAN_POINT('Origin',(-14.1247849194883,-25.3746234146051,16.));
#8963=CARTESIAN_POINT('',(-12.6247849194883,-25.3746234146051,10.));
#8964=CARTESIAN_POINT('',(-12.6247849194883,-25.3746234146051,16.));
#8965=CARTESIAN_POINT('Origin',(-14.1247849194883,-25.3746234146051,10.));
#8966=CARTESIAN_POINT('Origin',(-23.1247849194883,-6.37462341460511,15.7));
#8967=CARTESIAN_POINT('',(-21.6247849194883,-6.37462341460511,15.7));
#8968=CARTESIAN_POINT('Origin',(-21.3247849194883,-6.37462341460511,15.7));
#8969=CARTESIAN_POINT('Origin',(-23.1247849194883,-6.37462341460511,15.7));
#8970=CARTESIAN_POINT('Origin',(-23.1247849194883,-6.37462341460511,16.));
#8971=CARTESIAN_POINT('',(-21.6247849194883,-6.37462341460511,10.));
#8972=CARTESIAN_POINT('',(-21.6247849194883,-6.37462341460511,16.));
#8973=CARTESIAN_POINT('Origin',(-23.1247849194883,-6.37462341460511,10.));
#8974=CARTESIAN_POINT('Origin',(23.1247849194883,-6.37462341460511,15.7));
#8975=CARTESIAN_POINT('',(24.6247849194883,-6.37462341460511,15.7));
#8976=CARTESIAN_POINT('Origin',(24.9247849194883,-6.37462341460511,15.7));
#8977=CARTESIAN_POINT('Origin',(23.1247849194883,-6.37462341460511,15.7));
#8978=CARTESIAN_POINT('Origin',(23.1247849194883,-6.37462341460511,16.));
#8979=CARTESIAN_POINT('',(24.6247849194883,-6.37462341460511,10.));
#8980=CARTESIAN_POINT('',(24.6247849194883,-6.37462341460511,16.));
#8981=CARTESIAN_POINT('Origin',(23.1247849194883,-6.37462341460511,10.));
#8982=CARTESIAN_POINT('Origin',(14.1247849194883,-25.3746234146051,15.7));
#8983=CARTESIAN_POINT('',(15.6247849194883,-25.3746234146051,15.7));
#8984=CARTESIAN_POINT('Origin',(15.9247849194883,-25.3746234146051,15.7));
#8985=CARTESIAN_POINT('Origin',(14.1247849194883,-25.3746234146051,15.7));
#8986=CARTESIAN_POINT('Origin',(14.1247849194883,-25.3746234146051,16.));
#8987=CARTESIAN_POINT('',(15.6247849194883,-25.3746234146051,10.));
#8988=CARTESIAN_POINT('',(15.6247849194883,-25.3746234146051,16.));
#8989=CARTESIAN_POINT('Origin',(14.1247849194883,-25.3746234146051,10.));
#8990=CARTESIAN_POINT('Origin',(23.1247849194883,6.37462341460511,15.7));
#8991=CARTESIAN_POINT('',(24.6247849194883,6.37462341460511,15.7));
#8992=CARTESIAN_POINT('Origin',(24.9247849194883,6.37462341460511,15.7));
#8993=CARTESIAN_POINT('Origin',(23.1247849194883,6.37462341460511,15.7));
#8994=CARTESIAN_POINT('Origin',(23.1247849194883,6.37462341460511,16.));
#8995=CARTESIAN_POINT('',(24.6247849194883,6.37462341460511,10.));
#8996=CARTESIAN_POINT('',(24.6247849194883,6.37462341460511,16.));
#8997=CARTESIAN_POINT('Origin',(23.1247849194883,6.37462341460511,10.));
#8998=CARTESIAN_POINT('Origin',(23.1247849194883,15.3746234146051,15.7));
#8999=CARTESIAN_POINT('',(24.6247849194883,15.3746234146051,15.7));
#9000=CARTESIAN_POINT('Origin',(24.9247849194883,15.3746234146051,15.7));
#9001=CARTESIAN_POINT('Origin',(23.1247849194883,15.3746234146051,15.7));
#9002=CARTESIAN_POINT('Origin',(23.1247849194883,15.3746234146051,16.));
#9003=CARTESIAN_POINT('',(24.6247849194883,15.3746234146051,10.));
#9004=CARTESIAN_POINT('',(24.6247849194883,15.3746234146051,16.));
#9005=CARTESIAN_POINT('Origin',(23.1247849194883,15.3746234146051,10.));
#9006=CARTESIAN_POINT('Origin',(-23.1247849194883,-15.3746234146051,15.7));
#9007=CARTESIAN_POINT('',(-21.6247849194883,-15.3746234146051,15.7));
#9008=CARTESIAN_POINT('Origin',(-21.3247849194883,-15.3746234146051,15.7));
#9009=CARTESIAN_POINT('Origin',(-23.1247849194883,-15.3746234146051,15.7));
#9010=CARTESIAN_POINT('Origin',(-23.1247849194883,-15.3746234146051,16.));
#9011=CARTESIAN_POINT('',(-21.6247849194883,-15.3746234146051,10.));
#9012=CARTESIAN_POINT('',(-21.6247849194883,-15.3746234146051,16.));
#9013=CARTESIAN_POINT('Origin',(-23.1247849194883,-15.3746234146051,10.));
#9014=CARTESIAN_POINT('Origin',(-23.1247849194883,15.3746234146051,15.7));
#9015=CARTESIAN_POINT('',(-21.6247849194883,15.3746234146051,15.7));
#9016=CARTESIAN_POINT('Origin',(-21.3247849194883,15.3746234146051,15.7));
#9017=CARTESIAN_POINT('',(-23.1247849194883,13.8746234146051,15.7));
#9018=CARTESIAN_POINT('Origin',(-23.1247849194883,15.3746234146051,15.7));
#9019=CARTESIAN_POINT('Origin',(-23.1247849194883,15.3746234146051,15.7));
#9020=CARTESIAN_POINT('Origin',(-23.1247849194883,15.3746234146051,16.));
#9021=CARTESIAN_POINT('',(-23.1247849194883,13.8746234146051,10.));
#9022=CARTESIAN_POINT('',(-23.1247849194883,13.8746234146051,16.));
#9023=CARTESIAN_POINT('Origin',(-23.1247849194883,15.3746234146051,10.));
#9024=CARTESIAN_POINT('Origin',(-23.1247849194883,-25.3746234146051,15.7));
#9025=CARTESIAN_POINT('',(-21.6247849194883,-25.3746234146051,15.7));
#9026=CARTESIAN_POINT('Origin',(-21.3247849194883,-25.3746234146051,15.7));
#9027=CARTESIAN_POINT('Origin',(-23.1247849194883,-25.3746234146051,15.7));
#9028=CARTESIAN_POINT('Origin',(-23.1247849194883,-25.3746234146051,16.));
#9029=CARTESIAN_POINT('',(-21.6247849194883,-25.3746234146051,10.));
#9030=CARTESIAN_POINT('',(-21.6247849194883,-25.3746234146051,16.));
#9031=CARTESIAN_POINT('Origin',(-23.1247849194883,-25.3746234146051,10.));
#9032=CARTESIAN_POINT('Origin',(-23.1247849194883,6.37462341460511,15.7));
#9033=CARTESIAN_POINT('',(-21.6247849194883,6.37462341460511,15.7));
#9034=CARTESIAN_POINT('Origin',(-21.3247849194883,6.37462341460511,15.7));
#9035=CARTESIAN_POINT('',(-23.1247849194883,4.87462341460511,15.7));
#9036=CARTESIAN_POINT('Origin',(-23.1247849194883,6.37462341460511,15.7));
#9037=CARTESIAN_POINT('Origin',(-23.1247849194883,6.37462341460511,15.7));
#9038=CARTESIAN_POINT('Origin',(-23.1247849194883,6.37462341460511,16.));
#9039=CARTESIAN_POINT('',(-23.1247849194883,4.87462341460511,10.));
#9040=CARTESIAN_POINT('',(-23.1247849194883,4.87462341460511,16.));
#9041=CARTESIAN_POINT('Origin',(-23.1247849194883,6.37462341460511,10.));
#9042=CARTESIAN_POINT('Origin',(23.1247849194883,-15.3746234146051,15.7));
#9043=CARTESIAN_POINT('',(24.6247849194883,-15.3746234146051,15.7));
#9044=CARTESIAN_POINT('Origin',(24.9247849194883,-15.3746234146051,15.7));
#9045=CARTESIAN_POINT('Origin',(23.1247849194883,-15.3746234146051,15.7));
#9046=CARTESIAN_POINT('Origin',(23.1247849194883,-15.3746234146051,16.));
#9047=CARTESIAN_POINT('',(24.6247849194883,-15.3746234146051,10.));
#9048=CARTESIAN_POINT('',(24.6247849194883,-15.3746234146051,16.));
#9049=CARTESIAN_POINT('Origin',(23.1247849194883,-15.3746234146051,10.));
#9050=CARTESIAN_POINT('Origin',(14.1247849194883,25.3746234146051,15.7));
#9051=CARTESIAN_POINT('',(15.6247849194883,25.3746234146051,15.7));
#9052=CARTESIAN_POINT('Origin',(15.9247849194883,25.3746234146051,15.7));
#9053=CARTESIAN_POINT('Origin',(14.1247849194883,25.3746234146051,15.7));
#9054=CARTESIAN_POINT('Origin',(14.1247849194883,25.3746234146051,16.));
#9055=CARTESIAN_POINT('',(15.6247849194883,25.3746234146051,10.));
#9056=CARTESIAN_POINT('',(15.6247849194883,25.3746234146051,16.));
#9057=CARTESIAN_POINT('Origin',(14.1247849194883,25.3746234146051,10.));
#9058=CARTESIAN_POINT('Origin',(23.1247849194883,-25.3746234146051,15.7));
#9059=CARTESIAN_POINT('',(24.6247849194883,-25.3746234146051,15.7));
#9060=CARTESIAN_POINT('Origin',(24.9247849194883,-25.3746234146051,15.7));
#9061=CARTESIAN_POINT('Origin',(23.1247849194883,-25.3746234146051,15.7));
#9062=CARTESIAN_POINT('Origin',(23.1247849194883,-25.3746234146051,16.));
#9063=CARTESIAN_POINT('',(24.6247849194883,-25.3746234146051,10.));
#9064=CARTESIAN_POINT('',(24.6247849194883,-25.3746234146051,16.));
#9065=CARTESIAN_POINT('Origin',(23.1247849194883,-25.3746234146051,10.));
#9066=CARTESIAN_POINT('Origin',(23.1247849194883,25.3746234146051,15.7));
#9067=CARTESIAN_POINT('',(24.6247849194883,25.3746234146051,15.7));
#9068=CARTESIAN_POINT('Origin',(24.9247849194883,25.3746234146051,15.7));
#9069=CARTESIAN_POINT('Origin',(23.1247849194883,25.3746234146051,15.7));
#9070=CARTESIAN_POINT('Origin',(23.1247849194883,25.3746234146051,16.));
#9071=CARTESIAN_POINT('',(24.6247849194883,25.3746234146051,10.));
#9072=CARTESIAN_POINT('',(24.6247849194883,25.3746234146051,16.));
#9073=CARTESIAN_POINT('Origin',(23.1247849194883,25.3746234146051,10.));
#9074=CARTESIAN_POINT('Origin',(-23.1247849194883,25.3746234146051,15.7));
#9075=CARTESIAN_POINT('',(-21.6247849194883,25.3746234146051,15.7));
#9076=CARTESIAN_POINT('Origin',(-21.3247849194883,25.3746234146051,15.7));
#9077=CARTESIAN_POINT('Origin',(-23.1247849194883,25.3746234146051,15.7));
#9078=CARTESIAN_POINT('Origin',(-23.1247849194883,25.3746234146051,16.));
#9079=CARTESIAN_POINT('',(-21.6247849194883,25.3746234146051,10.));
#9080=CARTESIAN_POINT('',(-21.6247849194883,25.3746234146051,16.));
#9081=CARTESIAN_POINT('Origin',(-23.1247849194883,25.3746234146051,10.));
#9082=CARTESIAN_POINT('Origin',(-14.1247849194883,25.3746234146051,15.7));
#9083=CARTESIAN_POINT('',(-12.6247849194883,25.3746234146051,15.7));
#9084=CARTESIAN_POINT('Origin',(-12.3247849194883,25.3746234146051,15.7));
#9085=CARTESIAN_POINT('Origin',(-14.1247849194883,25.3746234146051,15.7));
#9086=CARTESIAN_POINT('Origin',(-14.1247849194883,25.3746234146051,16.));
#9087=CARTESIAN_POINT('',(-12.6247849194883,25.3746234146051,10.));
#9088=CARTESIAN_POINT('',(-12.6247849194883,25.3746234146051,16.));
#9089=CARTESIAN_POINT('Origin',(-14.1247849194883,25.3746234146051,10.));
#9090=CARTESIAN_POINT('Origin',(29.7,-15.,8.3));
#9091=CARTESIAN_POINT('',(29.7,-14.9999999999999,8.));
#9092=CARTESIAN_POINT('Origin',(29.7,-15.2999999999999,8.3));
#9093=CARTESIAN_POINT('',(29.7,14.9999999999999,8.));
#9094=CARTESIAN_POINT('',(29.7,-15.,8.));
#9095=CARTESIAN_POINT('Origin',(29.7,15.2999999999999,8.3));
#9096=CARTESIAN_POINT('Origin',(-29.7,-15.,8.3));
#9097=CARTESIAN_POINT('',(-29.7,14.9999999999999,8.));
#9098=CARTESIAN_POINT('Origin',(-29.7,15.2999999999999,8.3));
#9099=CARTESIAN_POINT('',(-29.7,-14.9999999999999,8.));
#9100=CARTESIAN_POINT('',(-29.7,-15.,8.));
#9101=CARTESIAN_POINT('Origin',(-29.7,-15.2999999999999,8.3));
#9102=CARTESIAN_POINT('Origin',(-29.7,15.2999999999999,10.));
#9103=CARTESIAN_POINT('',(-29.7,14.9999999999999,4.));
#9104=CARTESIAN_POINT('Origin',(-29.7,15.2999999999999,4.3));
#9105=CARTESIAN_POINT('',(-29.7,14.9999999999999,10.));
#9106=CARTESIAN_POINT('Origin',(29.7,-15.2999999999999,10.));
#9107=CARTESIAN_POINT('',(29.7,-14.9999999999999,4.));
#9108=CARTESIAN_POINT('Origin',(29.7,-15.2999999999999,4.3));
#9109=CARTESIAN_POINT('',(29.7,-14.9999999999999,10.));
#9110=CARTESIAN_POINT('Origin',(-29.7,7.49999999999996,4.3));
#9111=CARTESIAN_POINT('',(-29.7,15.9999999999999,4.));
#9112=CARTESIAN_POINT('Origin',(-29.7,16.2999999999999,4.3));
#9113=CARTESIAN_POINT('',(-29.7,7.49999999999996,4.));
#9114=CARTESIAN_POINT('Origin',(29.7,-7.49999999999996,4.3));
#9115=CARTESIAN_POINT('',(29.7,-15.9999999999999,4.));
#9116=CARTESIAN_POINT('Origin',(29.7,-16.2999999999999,4.3));
#9117=CARTESIAN_POINT('',(29.7,-7.49999999999996,4.));
#9118=CARTESIAN_POINT('Origin',(-29.7,-7.49999999999996,4.3));
#9119=CARTESIAN_POINT('',(-29.7,-14.9999999999999,4.));
#9120=CARTESIAN_POINT('',(-29.7,-15.9999999999999,4.));
#9121=CARTESIAN_POINT('',(-29.7,-7.49999999999996,4.));
#9122=CARTESIAN_POINT('Origin',(-29.7,-16.2999999999999,4.3));
#9123=CARTESIAN_POINT('Origin',(-29.7,-15.2999999999999,4.3));
#9124=CARTESIAN_POINT('Origin',(-29.7,16.2999999999999,8.));
#9125=CARTESIAN_POINT('',(-29.7,15.9999999999999,-7.85933214561696));
#9126=CARTESIAN_POINT('Origin',(-29.7,16.2999999999999,-7.55933214561695));
#9127=CARTESIAN_POINT('',(-29.7,15.9999999999999,8.));
#9128=CARTESIAN_POINT('Origin',(29.7,27.6999999999999,-7.55933214561695));
#9129=CARTESIAN_POINT('',(29.7,27.6999999999999,-7.85933214561696));
#9130=CARTESIAN_POINT('Origin',(29.7,27.6999999999999,-7.55933214561695));
#9131=CARTESIAN_POINT('',(29.7,27.9999999999999,-7.55933214561695));
#9132=CARTESIAN_POINT('Origin',(29.7,27.6999999999999,-7.55933214561695));
#9133=CARTESIAN_POINT('Origin',(29.7,27.6999999999999,-7.55933214561695));
#9134=CARTESIAN_POINT('Origin',(-29.7,27.6999999999999,-7.55933214561695));
#9135=CARTESIAN_POINT('',(-29.7,27.9999999999999,-7.55933214561695));
#9136=CARTESIAN_POINT('Origin',(-29.7,27.6999999999999,-7.55933214561695));
#9137=CARTESIAN_POINT('',(-29.7,27.6999999999999,-7.85933214561696));
#9138=CARTESIAN_POINT('Origin',(-29.7,27.6999999999999,-7.55933214561695));
#9139=CARTESIAN_POINT('Origin',(-29.7,27.6999999999999,-7.55933214561695));
#9140=CARTESIAN_POINT('Origin',(0.,27.6999999999999,-7.55933214561695));
#9141=CARTESIAN_POINT('',(0.,27.6999999999999,-7.85933214561696));
#9142=CARTESIAN_POINT('',(0.,27.9999999999999,-7.55933214561695));
#9143=CARTESIAN_POINT('Origin',(-29.7,7.99999999999996,-7.55933214561695));
#9144=CARTESIAN_POINT('',(-29.7,7.99999999999996,-7.85933214561696));
#9145=CARTESIAN_POINT('Origin',(29.7,-27.6999999999999,-7.55933214561695));
#9146=CARTESIAN_POINT('',(29.7,-27.6999999999999,-7.85933214561696));
#9147=CARTESIAN_POINT('',(29.7,-27.9999999999999,-7.55933214561695));
#9148=CARTESIAN_POINT('Origin',(29.7,-27.6999999999999,-7.55933214561695));
#9149=CARTESIAN_POINT('Origin',(29.7,-27.6999999999999,-7.55933214561695));
#9150=CARTESIAN_POINT('Origin',(29.7,-27.6999999999999,-7.55933214561695));
#9151=CARTESIAN_POINT('Origin',(29.7,-7.99999999999996,-7.55933214561695));
#9152=CARTESIAN_POINT('',(29.7,-15.9999999999999,-7.85933214561696));
#9153=CARTESIAN_POINT('',(29.7,-7.99999999999996,-7.85933214561696));
#9154=CARTESIAN_POINT('Origin',(29.7,-16.2999999999999,-7.55933214561695));
#9155=CARTESIAN_POINT('Origin',(29.7,28.2999999999999,3.7));
#9156=CARTESIAN_POINT('',(29.7,28.2999999999999,4.));
#9157=CARTESIAN_POINT('',(29.7,27.9999999999999,3.7));
#9158=CARTESIAN_POINT('Origin',(29.7,28.2999999999999,3.7));
#9159=CARTESIAN_POINT('Origin',(29.7,28.2999999999999,4.3));
#9160=CARTESIAN_POINT('Origin',(29.7,27.6999999999999,3.7));
#9161=CARTESIAN_POINT('Origin',(-29.7,-27.6999999999999,-7.55933214561695));
#9162=CARTESIAN_POINT('',(-29.7,-27.9999999999999,-7.55933214561695));
#9163=CARTESIAN_POINT('Origin',(-29.7,-27.6999999999999,-7.55933214561695));
#9164=CARTESIAN_POINT('',(-29.7,-27.6999999999999,-7.85933214561696));
#9165=CARTESIAN_POINT('Origin',(-29.7,-27.6999999999999,-7.55933214561695));
#9166=CARTESIAN_POINT('Origin',(-29.7,-27.6999999999999,-7.55933214561695));
#9167=CARTESIAN_POINT('Origin',(-29.7,-7.99999999999996,-7.55933214561695));
#9168=CARTESIAN_POINT('',(-29.7,-15.9999999999999,-7.85933214561696));
#9169=CARTESIAN_POINT('',(-29.7,-7.99999999999996,-7.85933214561696));
#9170=CARTESIAN_POINT('Origin',(-29.7,-16.2999999999999,-7.55933214561695));
#9171=CARTESIAN_POINT('Origin',(0.,-27.6999999999999,-7.55933214561695));
#9172=CARTESIAN_POINT('',(0.,-27.9999999999999,-7.55933214561695));
#9173=CARTESIAN_POINT('',(0.,-27.6999999999999,-7.85933214561696));
#9174=CARTESIAN_POINT('Origin',(-29.7,28.2999999999999,3.7));
#9175=CARTESIAN_POINT('',(-29.7,27.9999999999999,3.7));
#9176=CARTESIAN_POINT('',(-29.7,28.2999999999999,4.));
#9177=CARTESIAN_POINT('Origin',(-29.7,28.2999999999999,3.7));
#9178=CARTESIAN_POINT('Origin',(-29.7,27.6999999999999,3.7));
#9179=CARTESIAN_POINT('Origin',(-29.7,28.2999999999999,4.3));
#9180=CARTESIAN_POINT('Origin',(-29.7,27.6999999999999,2.07033392719152));
#9181=CARTESIAN_POINT('',(-29.7,27.9999999999999,2.07033392719152));
#9182=CARTESIAN_POINT('Origin',(29.7,-28.2999999999999,3.7));
#9183=CARTESIAN_POINT('',(29.7,-28.2999999999999,4.));
#9184=CARTESIAN_POINT('Origin',(29.7,-28.2999999999999,4.3));
#9185=CARTESIAN_POINT('',(29.7,-27.9999999999999,3.7));
#9186=CARTESIAN_POINT('Origin',(29.7,-28.2999999999999,3.7));
#9187=CARTESIAN_POINT('Origin',(29.7,-27.6999999999999,3.7));
#9188=CARTESIAN_POINT('Origin',(29.7,28.6999999999999,4.3));
#9189=CARTESIAN_POINT('',(29.7,28.6999999999999,4.));
#9190=CARTESIAN_POINT('Origin',(29.7,28.6999999999999,4.3));
#9191=CARTESIAN_POINT('',(29.7,28.9999999999999,4.3));
#9192=CARTESIAN_POINT('Origin',(29.7,28.6999999999999,4.3));
#9193=CARTESIAN_POINT('Origin',(29.7,28.6999999999999,4.3));
#9194=CARTESIAN_POINT('Origin',(-29.7,-28.2999999999999,3.7));
#9195=CARTESIAN_POINT('',(-29.7,-28.2999999999999,4.));
#9196=CARTESIAN_POINT('',(-29.7,-27.9999999999999,3.7));
#9197=CARTESIAN_POINT('Origin',(-29.7,-28.2999999999999,3.7));
#9198=CARTESIAN_POINT('Origin',(-29.7,-28.2999999999999,4.3));
#9199=CARTESIAN_POINT('Origin',(-29.7,-27.6999999999999,3.7));
#9200=CARTESIAN_POINT('Origin',(-29.7,28.6999999999999,4.3));
#9201=CARTESIAN_POINT('',(-29.7,28.9999999999999,4.3));
#9202=CARTESIAN_POINT('Origin',(-29.7,28.6999999999999,4.3));
#9203=CARTESIAN_POINT('',(-29.7,28.6999999999999,4.));
#9204=CARTESIAN_POINT('Origin',(-29.7,28.6999999999999,4.3));
#9205=CARTESIAN_POINT('Origin',(-29.7,28.6999999999999,4.3));
#9206=CARTESIAN_POINT('Origin',(0.,28.6999999999999,4.3));
#9207=CARTESIAN_POINT('',(0.,28.6999999999999,4.));
#9208=CARTESIAN_POINT('',(0.,28.9999999999999,4.3));
#9209=CARTESIAN_POINT('Origin',(-29.7,7.49999999999996,4.3));
#9210=CARTESIAN_POINT('',(-29.7,7.49999999999996,4.));
#9211=CARTESIAN_POINT('Origin',(29.7,-28.6999999999999,4.3));
#9212=CARTESIAN_POINT('',(29.7,-28.9999999999999,4.3));
#9213=CARTESIAN_POINT('Origin',(29.7,-28.6999999999999,4.3));
#9214=CARTESIAN_POINT('',(29.7,-28.6999999999999,4.));
#9215=CARTESIAN_POINT('Origin',(29.7,-28.6999999999999,4.3));
#9216=CARTESIAN_POINT('Origin',(29.7,-28.6999999999999,4.3));
#9217=CARTESIAN_POINT('Origin',(29.7,29.2999999999999,7.7));
#9218=CARTESIAN_POINT('',(29.7,29.2999999999999,8.));
#9219=CARTESIAN_POINT('',(29.7,28.9999999999999,7.7));
#9220=CARTESIAN_POINT('Origin',(29.7,29.2999999999999,7.7));
#9221=CARTESIAN_POINT('Origin',(29.7,29.2999999999999,8.3));
#9222=CARTESIAN_POINT('Origin',(29.7,28.6999999999999,7.7));
#9223=CARTESIAN_POINT('Origin',(-29.7,-28.6999999999999,4.3));
#9224=CARTESIAN_POINT('',(-29.7,-28.6999999999999,4.));
#9225=CARTESIAN_POINT('Origin',(-29.7,-28.6999999999999,4.3));
#9226=CARTESIAN_POINT('',(-29.7,-28.9999999999999,4.3));
#9227=CARTESIAN_POINT('Origin',(-29.7,-28.6999999999999,4.3));
#9228=CARTESIAN_POINT('Origin',(-29.7,-28.6999999999999,4.3));
#9229=CARTESIAN_POINT('Origin',(0.,-28.6999999999999,4.3));
#9230=CARTESIAN_POINT('',(0.,-28.9999999999999,4.3));
#9231=CARTESIAN_POINT('',(0.,-28.6999999999999,4.));
#9232=CARTESIAN_POINT('Origin',(-29.7,29.2999999999999,7.7));
#9233=CARTESIAN_POINT('',(-29.7,28.9999999999999,7.7));
#9234=CARTESIAN_POINT('',(-29.7,29.2999999999999,8.));
#9235=CARTESIAN_POINT('Origin',(-29.7,29.2999999999999,7.7));
#9236=CARTESIAN_POINT('Origin',(-29.7,28.6999999999999,7.7));
#9237=CARTESIAN_POINT('Origin',(-29.7,29.2999999999999,8.3));
#9238=CARTESIAN_POINT('Origin',(-29.7,28.6999999999999,8.));
#9239=CARTESIAN_POINT('',(-29.7,28.9999999999999,8.));
#9240=CARTESIAN_POINT('Origin',(29.7,-29.2999999999999,7.7));
#9241=CARTESIAN_POINT('',(29.7,-28.9999999999999,7.7));
#9242=CARTESIAN_POINT('',(29.7,-29.2999999999999,8.));
#9243=CARTESIAN_POINT('Origin',(29.7,-29.2999999999999,7.7));
#9244=CARTESIAN_POINT('Origin',(29.7,-28.6999999999999,7.7));
#9245=CARTESIAN_POINT('Origin',(29.7,-29.2999999999999,8.3));
#9246=CARTESIAN_POINT('Origin',(29.7,-28.6999999999999,8.));
#9247=CARTESIAN_POINT('',(29.7,-28.9999999999999,8.));
#9248=CARTESIAN_POINT('Origin',(29.7,29.7,8.3));
#9249=CARTESIAN_POINT('',(29.7,29.7,8.));
#9250=CARTESIAN_POINT('Origin',(29.7,29.7,8.3));
#9251=CARTESIAN_POINT('',(29.7,30.,8.3));
#9252=CARTESIAN_POINT('Origin',(29.7,29.7,8.3));
#9253=CARTESIAN_POINT('Origin',(29.7,29.7,8.3));
#9254=CARTESIAN_POINT('Origin',(-29.7,-29.2999999999999,7.7));
#9255=CARTESIAN_POINT('',(-29.7,-29.2999999999999,8.));
#9256=CARTESIAN_POINT('',(-29.7,-28.9999999999999,7.7));
#9257=CARTESIAN_POINT('Origin',(-29.7,-29.2999999999999,7.7));
#9258=CARTESIAN_POINT('Origin',(-29.7,-29.2999999999999,8.3));
#9259=CARTESIAN_POINT('Origin',(-29.7,-28.6999999999999,7.7));
#9260=CARTESIAN_POINT('Origin',(-29.7,29.7,8.3));
#9261=CARTESIAN_POINT('',(-29.7,30.,8.3));
#9262=CARTESIAN_POINT('Origin',(-29.7,29.7,8.3));
#9263=CARTESIAN_POINT('',(-29.7,29.7,8.));
#9264=CARTESIAN_POINT('Origin',(-29.7,29.7,8.3));
#9265=CARTESIAN_POINT('Origin',(-29.7,29.7,8.3));
#9266=CARTESIAN_POINT('Origin',(0.,29.7,8.3));
#9267=CARTESIAN_POINT('',(0.,29.7,8.));
#9268=CARTESIAN_POINT('',(0.,30.,8.3));
#9269=CARTESIAN_POINT('Origin',(-29.7,-15.,8.3));
#9270=CARTESIAN_POINT('',(-29.7,-15.,8.));
#9271=CARTESIAN_POINT('Origin',(29.7,-29.7,8.3));
#9272=CARTESIAN_POINT('',(29.7,-30.,8.3));
#9273=CARTESIAN_POINT('Origin',(29.7,-29.7,8.3));
#9274=CARTESIAN_POINT('',(29.7,-29.7,8.));
#9275=CARTESIAN_POINT('Origin',(29.7,-29.7,8.3));
#9276=CARTESIAN_POINT('Origin',(29.7,-29.7,8.3));
#9277=CARTESIAN_POINT('Origin',(29.7,29.7,15.7));
#9278=CARTESIAN_POINT('',(29.7,30.,15.7));
#9279=CARTESIAN_POINT('Origin',(29.7,29.7,15.7));
#9280=CARTESIAN_POINT('Origin',(29.7,29.7,15.7));
#9281=CARTESIAN_POINT('Origin',(29.7,29.7,15.7));
#9282=CARTESIAN_POINT('Origin',(-29.7,-29.7,8.3));
#9283=CARTESIAN_POINT('',(-29.7,-29.7,8.));
#9284=CARTESIAN_POINT('Origin',(-29.7,-29.7,8.3));
#9285=CARTESIAN_POINT('',(-29.7,-30.,8.3));
#9286=CARTESIAN_POINT('Origin',(-29.7,-29.7,8.3));
#9287=CARTESIAN_POINT('Origin',(-29.7,-29.7,8.3));
#9288=CARTESIAN_POINT('Origin',(0.,-29.7,8.3));
#9289=CARTESIAN_POINT('',(0.,-30.,8.3));
#9290=CARTESIAN_POINT('',(0.,-29.7,8.));
#9291=CARTESIAN_POINT('Origin',(-29.7,29.7,15.7));
#9292=CARTESIAN_POINT('Origin',(-29.7,29.7,15.7));
#9293=CARTESIAN_POINT('',(-29.7,30.,15.7));
#9294=CARTESIAN_POINT('Origin',(-29.7,29.7,15.7));
#9295=CARTESIAN_POINT('Origin',(-29.7,29.7,15.7));
#9296=CARTESIAN_POINT('Origin',(0.,29.7,15.7));
#9297=CARTESIAN_POINT('',(0.,30.,15.7));
#9298=CARTESIAN_POINT('Origin',(-29.7,29.7,10.));
#9299=CARTESIAN_POINT('',(-29.7,30.,10.));
#9300=CARTESIAN_POINT('Origin',(29.7,-29.7,15.7));
#9301=CARTESIAN_POINT('Origin',(29.7,-29.7,15.7));
#9302=CARTESIAN_POINT('',(29.7,-30.,15.7));
#9303=CARTESIAN_POINT('Origin',(29.7,-29.7,15.7));
#9304=CARTESIAN_POINT('Origin',(29.7,-29.7,15.7));
#9305=CARTESIAN_POINT('Origin',(-29.7,-29.7,15.7));
#9306=CARTESIAN_POINT('',(-29.7,-30.,15.7));
#9307=CARTESIAN_POINT('Origin',(-29.7,-29.7,15.7));
#9308=CARTESIAN_POINT('Origin',(-29.7,-29.7,15.7));
#9309=CARTESIAN_POINT('Origin',(-29.7,-29.7,15.7));
#9310=CARTESIAN_POINT('Origin',(0.,-29.7,15.7));
#9311=CARTESIAN_POINT('',(0.,-30.,15.7));
#9312=CARTESIAN_POINT('Origin',(-29.7,15.,15.7));
#9313=CARTESIAN_POINT('Origin',(-29.7,-29.7,14.));
#9314=CARTESIAN_POINT('',(-29.7,-30.,14.));
#9315=CARTESIAN_POINT('Origin',(29.7,-29.7,14.));
#9316=CARTESIAN_POINT('',(29.7,-30.,14.));
#9317=CARTESIAN_POINT('Origin',(29.7,15.,15.7));
#9318=CARTESIAN_POINT('Origin',(-29.7,-15.,8.3));
#9319=CARTESIAN_POINT('',(-29.7,-15.,8.));
#9320=CARTESIAN_POINT('Origin',(29.7,29.7,10.));
#9321=CARTESIAN_POINT('',(29.7,30.,10.));
#9322=CARTESIAN_POINT('Origin',(29.7,-15.,8.3));
#9323=CARTESIAN_POINT('',(29.7,-15.,8.));
#9324=CARTESIAN_POINT('Origin',(-29.7,-28.6999999999999,8.));
#9325=CARTESIAN_POINT('',(-29.7,-28.9999999999999,8.));
#9326=CARTESIAN_POINT('Origin',(0.,-29.2999999999999,7.7));
#9327=CARTESIAN_POINT('',(0.,-29.2999999999999,8.));
#9328=CARTESIAN_POINT('',(0.,-28.9999999999999,7.7));
#9329=CARTESIAN_POINT('Origin',(29.7,-15.,8.3));
#9330=CARTESIAN_POINT('',(29.7,-15.,8.));
#9331=CARTESIAN_POINT('Origin',(0.,29.2999999999999,7.7));
#9332=CARTESIAN_POINT('',(0.,29.2999999999999,8.));
#9333=CARTESIAN_POINT('',(0.,28.9999999999999,7.7));
#9334=CARTESIAN_POINT('Origin',(-29.7,-7.49999999999996,4.3));
#9335=CARTESIAN_POINT('',(-29.7,-7.49999999999996,4.));
#9336=CARTESIAN_POINT('Origin',(29.7,28.6999999999999,8.));
#9337=CARTESIAN_POINT('',(29.7,28.9999999999999,8.));
#9338=CARTESIAN_POINT('Origin',(29.7,-7.49999999999996,4.3));
#9339=CARTESIAN_POINT('',(29.7,-7.49999999999996,4.));
#9340=CARTESIAN_POINT('Origin',(-29.7,-27.6999999999999,2.07033392719152));
#9341=CARTESIAN_POINT('',(-29.7,-27.9999999999999,2.07033392719152));
#9342=CARTESIAN_POINT('Origin',(0.,-28.2999999999999,3.7));
#9343=CARTESIAN_POINT('',(0.,-28.2999999999999,4.));
#9344=CARTESIAN_POINT('',(0.,-27.9999999999999,3.7));
#9345=CARTESIAN_POINT('Origin',(29.7,7.49999999999996,4.3));
#9346=CARTESIAN_POINT('',(29.7,7.49999999999996,4.));
#9347=CARTESIAN_POINT('Origin',(29.7,-27.6999999999999,2.07033392719152));
#9348=CARTESIAN_POINT('',(29.7,-27.9999999999999,2.07033392719152));
#9349=CARTESIAN_POINT('Origin',(0.,28.2999999999999,3.7));
#9350=CARTESIAN_POINT('',(0.,28.2999999999999,4.));
#9351=CARTESIAN_POINT('',(0.,27.9999999999999,3.7));
#9352=CARTESIAN_POINT('Origin',(29.7,27.6999999999999,2.07033392719152));
#9353=CARTESIAN_POINT('',(29.7,27.9999999999999,2.07033392719152));
#9354=CARTESIAN_POINT('Origin',(-29.7,-16.2999999999999,8.));
#9355=CARTESIAN_POINT('',(-29.7,-15.9999999999999,8.));
#9356=CARTESIAN_POINT('Origin',(29.7,7.99999999999996,-7.55933214561695));
#9357=CARTESIAN_POINT('',(29.7,15.9999999999999,-7.85933214561696));
#9358=CARTESIAN_POINT('',(29.7,7.99999999999996,-7.85933214561696));
#9359=CARTESIAN_POINT('Origin',(29.7,16.2999999999999,-7.55933214561695));
#9360=CARTESIAN_POINT('Origin',(29.7,-16.2999999999999,8.));
#9361=CARTESIAN_POINT('',(29.7,-15.9999999999999,8.));
#9362=CARTESIAN_POINT('Origin',(29.7,16.2999999999999,8.));
#9363=CARTESIAN_POINT('',(29.7,15.9999999999999,4.));
#9364=CARTESIAN_POINT('',(29.7,15.9999999999999,8.));
#9365=CARTESIAN_POINT('Origin',(29.7,16.2999999999999,4.3));
#9366=CARTESIAN_POINT('Origin',(-29.7,-15.2999999999999,10.));
#9367=CARTESIAN_POINT('',(-29.7,-14.9999999999999,10.));
#9368=CARTESIAN_POINT('Origin',(29.7,7.49999999999996,4.3));
#9369=CARTESIAN_POINT('',(29.7,14.9999999999999,4.));
#9370=CARTESIAN_POINT('',(29.7,7.49999999999996,4.));
#9371=CARTESIAN_POINT('Origin',(29.7,15.2999999999999,4.3));
#9372=CARTESIAN_POINT('Origin',(29.7,15.2999999999999,10.));
#9373=CARTESIAN_POINT('',(29.7,14.9999999999999,10.));
#9374=CARTESIAN_POINT('Origin',(0.,15.9999999999999,4.));
#9375=CARTESIAN_POINT('',(0.,15.9999999999999,4.));
#9376=CARTESIAN_POINT('',(0.,15.9999999999999,-7.85933214561696));
#9377=CARTESIAN_POINT('Origin',(0.,14.9999999999999,4.));
#9378=CARTESIAN_POINT('',(0.,14.9999999999999,4.));
#9379=CARTESIAN_POINT('Origin',(0.,14.9999999999999,8.));
#9380=CARTESIAN_POINT('',(0.,14.9999999999999,8.));
#9381=CARTESIAN_POINT('Origin',(0.,-30.,8.));
#9382=CARTESIAN_POINT('',(0.,-14.9999999999999,8.));
#9383=CARTESIAN_POINT('Origin',(0.,-14.9999999999999,8.));
#9384=CARTESIAN_POINT('',(0.,-14.9999999999999,4.));
#9385=CARTESIAN_POINT('Origin',(0.,-15.9999999999999,-7.85933214561696));
#9386=CARTESIAN_POINT('',(0.,-15.9999999999999,-7.85933214561696));
#9387=CARTESIAN_POINT('Origin',(0.,-14.9999999999999,4.));
#9388=CARTESIAN_POINT('',(0.,-15.9999999999999,4.));
#9389=CARTESIAN_POINT('Origin',(0.,-15.9999999999999,4.));
#9390=CARTESIAN_POINT('Origin',(0.,27.9999999999999,-7.85933214561696));
#9391=CARTESIAN_POINT('Origin',(0.,-27.9999999999999,-7.85933214561696));
#9392=CARTESIAN_POINT('Origin',(0.,14.9999999999999,4.));
#9393=CARTESIAN_POINT('Origin',(0.,28.9999999999999,4.));
#9394=CARTESIAN_POINT('Origin',(0.,-14.9999999999999,4.));
#9395=CARTESIAN_POINT('Origin',(0.,-28.9999999999999,4.));
#9396=CARTESIAN_POINT('Origin',(0.,-30.,8.));
#9397=CARTESIAN_POINT('Origin',(0.,-30.,8.));
#9398=CARTESIAN_POINT('Origin',(0.,30.,8.));
#9399=CARTESIAN_POINT('Origin',(0.,-30.,16.));
#9400=CARTESIAN_POINT('Origin',(0.,15.9999999999999,-7.85933214561696));
#9401=CARTESIAN_POINT('Origin',(-14.1247849194883,-25.3746234146051,10.));
#9402=CARTESIAN_POINT('Origin',(-23.1247849194883,-6.37462341460511,10.));
#9403=CARTESIAN_POINT('Origin',(23.1247849194883,-6.37462341460511,10.));
#9404=CARTESIAN_POINT('Origin',(14.1247849194883,-25.3746234146051,10.));
#9405=CARTESIAN_POINT('Origin',(23.1247849194883,6.37462341460511,10.));
#9406=CARTESIAN_POINT('Origin',(23.1247849194883,15.3746234146051,10.));
#9407=CARTESIAN_POINT('Origin',(-23.1247849194883,-15.3746234146051,10.));
#9408=CARTESIAN_POINT('Origin',(-23.1247849194883,15.3746234146051,10.));
#9409=CARTESIAN_POINT('Origin',(-23.1247849194883,-25.3746234146051,10.));
#9410=CARTESIAN_POINT('Origin',(-23.1247849194883,6.37462341460511,10.));
#9411=CARTESIAN_POINT('Origin',(23.1247849194883,-15.3746234146051,10.));
#9412=CARTESIAN_POINT('Origin',(14.1247849194883,25.3746234146051,10.));
#9413=CARTESIAN_POINT('Origin',(23.1247849194883,-25.3746234146051,10.));
#9414=CARTESIAN_POINT('Origin',(23.1247849194883,25.3746234146051,10.));
#9415=CARTESIAN_POINT('Origin',(-23.1247849194883,25.3746234146051,10.));
#9416=CARTESIAN_POINT('Origin',(-14.1247849194883,25.3746234146051,10.));
#10617=UNCERTAINTY_MEASURE_WITH_UNIT(LENGTH_MEASURE(0.01),#10640,
'DISTANCE_ACCURACY_VALUE',
'Maximum model space distance between geometric entities at asserted c
onnectivities');
#10627=UNCERTAINTY_MEASURE_WITH_UNIT(LENGTH_MEASURE(0.01),#10640,
'DISTANCE_ACCURACY_VALUE',
'Maximum model space distance between geometric entities at asserted c
onnectivities');
#10629=(
GEOMETRIC_REPRESENTATION_CONTEXT(3)
GLOBAL_UNCERTAINTY_ASSIGNED_CONTEXT((#10617))
GLOBAL_UNIT_ASSIGNED_CONTEXT((#10640,#10642,#10643))
REPRESENTATION_CONTEXT('','3D')
);
#10639=(
GEOMETRIC_REPRESENTATION_CONTEXT(3)
GLOBAL_UNCERTAINTY_ASSIGNED_CONTEXT((#10627))
GLOBAL_UNIT_ASSIGNED_CONTEXT((#10640,#10642,#10643))
REPRESENTATION_CONTEXT('','3D')
);
#10640=(
LENGTH_UNIT()
NAMED_UNIT(*)
SI_UNIT(.MILLI.,.METRE.)
);
#10642=(
NAMED_UNIT(*)
PLANE_ANGLE_UNIT()
SI_UNIT($,.RADIAN.)
);
#10643=(
NAMED_UNIT(*)
SI_UNIT($,.STERADIAN.)
SOLID_ANGLE_UNIT()
);
#10645=SHAPE_DEFINITION_REPRESENTATION(#10656,#10677);
#10656=PRODUCT_DEFINITION_SHAPE('',$,#10689);
#10677=SHAPE_REPRESENTATION('',(#5835),#10629);
#10687=PRODUCT_DEFINITION_CONTEXT('part definition',#10722,'design');
#10689=PRODUCT_DEFINITION('Base','Base',#10700,#10687);
#10700=PRODUCT_DEFINITION_FORMATION('',$,#10725);
#10722=APPLICATION_CONTEXT(
'Core Data for Automotive Mechanical Design Process');
#10723=PRODUCT_CONTEXT('part definition',#10722,'mechanical');
#10725=PRODUCT('Base','Base',$,(#10723));
#10763=COLOUR_RGB('Dark Blue',0.08,0.2,0.34);
#10764=FILL_AREA_STYLE_COLOUR('',#10763);
#10765=FILL_AREA_STYLE('',(#10764));
#10766=SURFACE_STYLE_FILL_AREA(#10765);
#10767=SURFACE_SIDE_STYLE('',(#10766));
#10768=SURFACE_STYLE_USAGE(.BOTH.,#10767);
#10769=PRESENTATION_STYLE_ASSIGNMENT((#10768));
ENDSEC;
END-ISO-10303-21;
